ISO-10303-21;
HEADER;
FILE_DESCRIPTION (('STEP AP214'),
    '1' );
FILE_NAME ('hex nut gradec_iso_ISO - 4034 - M5 - N.step',
    '2026-10-08T08:02:49',
    ( '' ),
    ( '' ),
    'SwSTEP 2.0',
    'SolidWorks 2026',
    '' );
FILE_SCHEMA (( 'AUTOMOTIVE_DESIGN' ));
ENDSEC;

DATA;
#70=EDGE_LOOP ( 'NONE', ( #37119, #28268, #15345 ) ) ;
#203=CARTESIAN_POINT ( 'NONE',  ( -2.678494666091065124, -3.072372537026387018, -0.03421028094655000767 ) ) ;
#331=VERTEX_POINT ( 'NONE', #19436 ) ;
#393=DIRECTION ( 'NONE',  ( -1.000000000000000000, 0.000000000000000000, 0.000000000000000000 ) ) ;
#478=VERTEX_POINT ( 'NONE', #23060 ) ;
#503=LINE ( 'NONE', #38764, #11349 ) ;
#509=SURFACE_STYLE_USAGE ( .BOTH. , #19650 ) ;
#776=ADVANCED_FACE ( 'NONE', ( #3231 ), #27365, .T. ) ;
#777=CARTESIAN_POINT ( 'NONE',  ( -4.000000000000000000, -0.3902508023145539462, 2.371692252312039717E-17 ) ) ;
#849=CARTESIAN_POINT ( 'NONE',  ( 3.345653888883671545, -2.687187980154741140, -5.460849780464844372 ) ) ;
#1062=CARTESIAN_POINT ( 'NONE',  ( 0.000000000000000000, 0.000000000000000000, -5.599999999999999645 ) ) ;
#1173=ORIENTED_EDGE ( 'NONE', *, *, #12970, .F. ) ;
#1181=DIRECTION ( 'NONE',  ( 1.000000000000000000, 0.000000000000000000, 0.000000000000000000 ) ) ;
#1253=CARTESIAN_POINT ( 'NONE',  ( 0.000000000000000000, 0.000000000000000000, 0.000000000000000000 ) ) ;
#1445=CARTESIAN_POINT ( 'NONE',  ( -2.500000000000000444, 3.061616997868384127E-16, 3.469446951953614189E-15 ) ) ;
#1449=AXIS2_PLACEMENT_3D ( 'NONE', #48895, #15398, #34502 ) ;
#1465=CARTESIAN_POINT ( 'NONE',  ( -2.678494666091065124, -3.072372537026387018, -5.565789719053451101 ) ) ;
#1479=CARTESIAN_POINT ( 'NONE',  ( -4.000000000000000000, -2.309401076758531346, -0.3572655899081733644 ) ) ;
#1556=FACE_OUTER_BOUND ( 'NONE', #17373, .T. ) ;
#1588=CONICAL_SURFACE ( 'NONE', #36650, 4.000000000000000000, 1.047197551196595855 ) ;
#1614=CARTESIAN_POINT ( 'NONE',  ( -2.000000000000022649, -3.464101615137742396, 0.000000000000000000 ) ) ;
#1615=VECTOR ( 'NONE', #23772, 1000.000000000000000 ) ;
#1701=DIRECTION ( 'NONE',  ( -1.000000000000000000, 0.000000000000000000, 0.000000000000000000 ) ) ;
#1798=ORIENTED_EDGE ( 'NONE', *, *, #49935, .T. ) ;
#1872=DIRECTION ( 'NONE',  ( 0.000000000000000000, 0.000000000000000000, -1.000000000000000000 ) ) ;
#1947=VERTEX_POINT ( 'NONE', #27183 ) ;
#2011=CARTESIAN_POINT ( 'NONE',  ( 0.000000000000000000, 0.000000000000000000, 0.000000000000000000 ) ) ;
#2021=AXIS2_PLACEMENT_3D ( 'NONE', #34926, #30197, #50237 ) ;
#2062=DIRECTION ( 'NONE',  ( -1.000000000000000000, 0.000000000000000000, 0.000000000000000000 ) ) ;
#2126=CARTESIAN_POINT ( 'NONE',  ( -4.000000000000000000, 2.309401076758496263, -0.3572655899081631503 ) ) ;
#2128=EDGE_CURVE ( 'NONE', #48540, #52878, #3114, .T. ) ;
#2137=B_SPLINE_CURVE_WITH_KNOTS ( 'NONE', 3,
 ( #57787, #10203, #29299, #48410 ),
 .UNSPECIFIED., .F., .F.,
 ( 4, 4 ),
 ( 2.380737581782212780E-07, 0.002336974151641539946 ),
 .UNSPECIFIED. ) ;
#2154=B_SPLINE_CURVE_WITH_KNOTS ( 'NONE', 3,
 ( #7739, #39367, #9594, #4881, #19636, #5188 ),
 .UNSPECIFIED., .F., .F.,
 ( 4, 2, 4 ),
 ( 0.004120275011746849653, 0.005288420935197133549, 0.006456566858647416578 ),
 .UNSPECIFIED. ) ;
#2249=AXIS2_PLACEMENT_3D ( 'NONE', #25761, #35180, #20447 ) ;
#2295=AXIS2_PLACEMENT_3D ( 'NONE', #33150, #28123, #47242 ) ;
#2296=UNCERTAINTY_MEASURE_WITH_UNIT (LENGTH_MEASURE( 1.000000000000000082E-05 ), #22184, 'distance_accuracy_value', 'NONE');
#2324=CARTESIAN_POINT ( 'NONE',  ( 0.000000000000000000, 0.000000000000000000, -5.600000000000000533 ) ) ;
#2422=CARTESIAN_POINT ( 'NONE',  ( -0.6554360035617894376, 4.240386000424038571, -0.1586754815284913411 ) ) ;
#2494=CIRCLE ( 'NONE', #56508, 2.099999999999999645 ) ;
#2681=ORIENTED_EDGE ( 'NONE', *, *, #38988, .T. ) ;
#2703=AXIS2_PLACEMENT_3D ( 'NONE', #8726, #28143, #42892 ) ;
#2755=EDGE_CURVE ( 'NONE', #14506, #56562, #60466, .T. ) ;
#2845=ORIENTED_EDGE ( 'NONE', *, *, #22515, .F. ) ;
#2919=DIRECTION ( 'NONE',  ( 1.000000000000000000, 0.000000000000000000, 0.000000000000000000 ) ) ;
#3027=VERTEX_POINT ( 'NONE', #34143 ) ;
#3088=CARTESIAN_POINT ( 'NONE',  ( 2.099999999999999645, 0.000000000000000000, -0.2800830152838832965 ) ) ;
#3114=CIRCLE ( 'NONE', #43172, 2.099999999999999645 ) ;
#3178=DIRECTION ( 'NONE',  ( 0.5000000000000025535, -0.8660254037844371533, 0.000000000000000000 ) ) ;
#3231=FACE_OUTER_BOUND ( 'NONE', #60539, .T. ) ;
#3237=EDGE_CURVE ( 'NONE', #48540, #19953, #18978, .T. ) ;
#3274=AXIS2_PLACEMENT_3D ( 'NONE', #25580, #20889, #2062 ) ;
#3276=PRODUCT_CONTEXT ( 'NONE', #17150, 'mechanical' ) ;
#3310=SURFACE_SIDE_STYLE ('',( #41263 ) ) ;
#3326=DIRECTION ( 'NONE',  ( -0.000000000000000000, -0.000000000000000000, 1.000000000000000000 ) ) ;
#3372=EDGE_CURVE ( 'NONE', #44297, #47052, #32916, .T. ) ;
#3418=B_SPLINE_CURVE_WITH_KNOTS ( 'NONE', 3,
 ( #2126, #44783, #25035, #53819 ),
 .UNSPECIFIED., .F., .F.,
 ( 4, 4 ),
 ( 2.380737581620991176E-07, 0.002336974151641539946 ),
 .UNSPECIFIED. ) ;
#3425=CONICAL_SURFACE ( 'NONE', #38477, 2.500000000000002220, 0.9599310885968777018 ) ;
#3458=EDGE_LOOP ( 'NONE', ( #18223, #12423, #55653, #51690 ) ) ;
#3547=ORIENTED_EDGE ( 'NONE', *, *, #23484, .F. ) ;
#3759=CARTESIAN_POINT ( 'NONE',  ( 0.000000000000000000, 0.000000000000000000, 0.000000000000000000 ) ) ;
#4082=EDGE_CURVE ( 'NONE', #46482, #1947, #14121, .T. ) ;
#4274=SHAPE_REPRESENTATION_RELATIONSHIP ( 'NONE' , 'NONE' ,  #53251, #33281 ) ;
#4557=ADVANCED_FACE ( 'NONE', ( #54917 ), #56048, .F. ) ;
#4563=CARTESIAN_POINT ( 'NONE',  ( -2.000000000000022649, -3.464101615137742396, 0.000000000000000000 ) ) ;
#4588=CARTESIAN_POINT ( 'NONE',  ( -4.000000000000000000, -2.309401076758531346, -0.3572655899081733644 ) ) ;
#4661=EDGE_LOOP ( 'NONE', ( #53308, #17039 ) ) ;
#4834=ORIENTED_EDGE ( 'NONE', *, *, #10534, .T. ) ;
#4881=CARTESIAN_POINT ( 'NONE',  ( 4.000000000000003553, -0.7779732554280839318, -0.03354435108168055818 ) ) ;
#4909=CARTESIAN_POINT ( 'NONE',  ( 0.000000000000000000, 0.000000000000000000, -5.600000000000000533 ) ) ;
#5032=AXIS2_PLACEMENT_3D ( 'NONE', #48345, #5404, #393 ) ;
#5039=ADVANCED_FACE ( 'NONE', ( #32925 ), #24119, .T. ) ;
#5075=DIRECTION ( 'NONE',  ( 1.000000000000000000, 0.000000000000000000, 0.000000000000000000 ) ) ;
#5188=CARTESIAN_POINT ( 'NONE',  ( 4.000000000000000000, 0.000000000000000000, 0.000000000000000000 ) ) ;
#5205=FILL_AREA_STYLE_COLOUR ( '', #25905 ) ;
#5404=DIRECTION ( 'NONE',  ( 0.000000000000000000, 0.000000000000000000, -1.000000000000000000 ) ) ;
#5490=CARTESIAN_POINT ( 'NONE',  ( 0.6554360035617802227, -4.240386000424091861, -5.441324518471480687 ) ) ;
#5554=ORIENTED_EDGE ( 'NONE', *, *, #37422, .F. ) ;
#5573=CARTESIAN_POINT ( 'NONE',  ( 1.214306433183764966E-14, 4.618802153517020059, -5.599999999999999645 ) ) ;
#5673=ORIENTED_EDGE ( 'NONE', *, *, #2755, .F. ) ;
#5719=AXIS2_PLACEMENT_3D ( 'NONE', #43668, #42731, #38966 ) ;
#5783=ORIENTED_EDGE ( 'NONE', *, *, #54717, .T. ) ;
#5907=DIRECTION ( 'NONE',  ( -0.8660254037844348218, 0.5000000000000066613, 0.000000000000000000 ) ) ;
#5940=FACE_OUTER_BOUND ( 'NONE', #42713, .T. ) ;
#5977=ORIENTED_EDGE ( 'NONE', *, *, #48509, .F. ) ;
#6064=CARTESIAN_POINT ( 'NONE',  ( -4.000000000000000000, -0.7779732554280792689, -0.03354435108167819896 ) ) ;
#6107=CARTESIAN_POINT ( 'NONE',  ( 0.000000000000000000, 0.000000000000000000, 0.000000000000000000 ) ) ;
#6257=DIRECTION ( 'NONE',  ( 1.000000000000000000, 0.000000000000000000, 0.000000000000000000 ) ) ;
#6340=CARTESIAN_POINT ( 'NONE',  ( 1.321505333908968627, -3.855830693249186147, -0.03421028094655685636 ) ) ;
#6525=AXIS2_PLACEMENT_3D ( 'NONE', #24205, #52704, #5075 ) ;
#6602=B_SPLINE_CURVE_WITH_KNOTS ( 'NONE', 3,
 ( #12924, #40827, #13221, #32020 ),
 .UNSPECIFIED., .F., .F.,
 ( 4, 4 ),
 ( 2.380737581618737539E-07, 0.002336974151641576809 ),
 .UNSPECIFIED. ) ;
#6723=CARTESIAN_POINT ( 'NONE',  ( -4.000000000000000000, 2.309401076758531346, -5.242734410091827613 ) ) ;
#6786=VERTEX_POINT ( 'NONE', #39336 ) ;
#6872=MECHANICAL_DESIGN_GEOMETRIC_PRESENTATION_REPRESENTATION('',(#35892),#28889);
#6873=DIRECTION ( 'NONE',  ( -1.000000000000000000, 0.000000000000000000, 0.000000000000000000 ) ) ;
#7110=CARTESIAN_POINT ( 'NONE',  ( -2.000000000000009770, 3.464101615137749057, 0.000000000000000000 ) ) ;
#7204=FACE_OUTER_BOUND ( 'NONE', #32068, .T. ) ;
#7214=CIRCLE ( 'NONE', #2249, 4.000000000000000888 ) ;
#7234=ORIENTED_EDGE ( 'NONE', *, *, #55075, .T. ) ;
#7269=CIRCLE ( 'NONE', #9306, 4.000000000000000000 ) ;
#7376=B_SPLINE_CURVE_WITH_KNOTS ( 'NONE', 3,
 ( #60916, #13332, #6340, #34591, #10471, #29873 ),
 .UNSPECIFIED., .F., .F.,
 ( 4, 2, 4 ),
 ( 0.002336974151641521731, 0.003500975885716455828, 0.004664977619791389925 ),
 .UNSPECIFIED. ) ;
#7395=CARTESIAN_POINT ( 'NONE',  ( -4.000000000000000000, -2.309401076758531346, -5.242734410091827613 ) ) ;
#7456=B_SPLINE_CURVE_WITH_KNOTS ( 'NONE', 3,
 ( #57213, #9626, #203, #51922, #32843, #4588 ),
 .UNSPECIFIED., .F., .F.,
 ( 4, 2, 4 ),
 ( 0.002336974151641604130, 0.003500975885716476211, 0.004664977619791348291 ),
 .UNSPECIFIED. ) ;
#7477=CONICAL_SURFACE ( 'NONE', #37537, 4.000000000000000000, 1.047197551196595855 ) ;
#7489=EDGE_CURVE ( 'NONE', #26742, #14506, #31203, .T. ) ;
#7557=ADVANCED_FACE ( 'NONE', ( #19074 ), #47566, .F. ) ;
#7613=VERTEX_POINT ( 'NONE', #9644 ) ;
#7616=AXIS2_PLACEMENT_3D ( 'NONE', #40144, #1872, #11607 ) ;
#7709=SURFACE_STYLE_USAGE ( .BOTH. , #3310 ) ;
#7739=CARTESIAN_POINT ( 'NONE',  ( 3.999999999999990674, -2.309401076758548221, -0.3572655899081733644 ) ) ;
#7748=MANIFOLD_SOLID_BREP ( 'EndChamfer', #59047 ) ;
#7776=CARTESIAN_POINT ( 'NONE',  ( -4.000000000000000000, 1.557668341133497059, -0.1596965656957516910 ) ) ;
#7880=CARTESIAN_POINT ( 'NONE',  ( 4.000000000000002665, 1.557668341133517043, -5.440303434304241570 ) ) ;
#7925=CARTESIAN_POINT ( 'NONE',  ( 4.000000000000004441, -1.549102112939112486, -5.442104661404058241 ) ) ;
#7941=ORIENTED_EDGE ( 'NONE', *, *, #45929, .T. ) ;
#7970=CARTESIAN_POINT ( 'NONE',  ( -2.000000000000022649, -3.464101615137742396, -5.600000000000000533 ) ) ;
#7999=CARTESIAN_POINT ( 'NONE',  ( 2.000000000000010658, -3.464101615137748169, 0.000000000000000000 ) ) ;
#8202=ORIENTED_EDGE ( 'NONE', *, *, #4082, .T. ) ;
#8268=LINE ( 'NONE', #32412, #27407 ) ;
#8289=CONICAL_SURFACE ( 'NONE', #2295, 4.000000000000000000, 1.047197551196595855 ) ;
#8338=DIRECTION ( 'NONE',  ( -1.000000000000000000, 0.000000000000000000, 0.000000000000000000 ) ) ;
#8391=EDGE_CURVE ( 'NONE', #41414, #60958, #35541, .T. ) ;
#8466=VECTOR ( 'NONE', #50802, 1000.000000000000000 ) ;
#8624=AXIS2_PLACEMENT_3D ( 'NONE', #54825, #11961, #35134 ) ;
#8726=CARTESIAN_POINT ( 'NONE',  ( 0.000000000000000000, 0.000000000000000000, 0.000000000000000000 ) ) ;
#8801=ORIENTED_EDGE ( 'NONE', *, *, #40023, .F. ) ;
#8814=PRODUCT_DEFINITION ( 'UNKNOWN', '', #18901, #17974 ) ;
#8972=CARTESIAN_POINT ( 'NONE',  ( 4.000000000000003553, 2.309401076758524685, -0.3572655899081733644 ) ) ;
#9076=B_SPLINE_CURVE_WITH_KNOTS ( 'NONE', 3,
 ( #7110, #23023, #27711, #2422, #21548, #16866 ),
 .UNSPECIFIED., .F., .F.,
 ( 4, 2, 4 ),
 ( 0.002336974151641539946, 0.003500975885716448889, 0.004664977619791357832 ),
 .UNSPECIFIED. ) ;
#9083=CARTESIAN_POINT ( 'NONE',  ( 3.344563996438205677, 2.687817229851463097, -0.1586754815284831532 ) ) ;
#9100=ORIENTED_EDGE ( 'NONE', *, *, #49370, .F. ) ;
#9165=UNCERTAINTY_MEASURE_WITH_UNIT (LENGTH_MEASURE( 1.000000000000000082E-05 ), #26832, 'distance_accuracy_value', 'NONE');
#9231=EDGE_CURVE ( 'NONE', #3027, #51786, #36424, .T. ) ;
#9304=SURFACE_STYLE_FILL_AREA ( #10241 ) ;
#9306=AXIS2_PLACEMENT_3D ( 'NONE', #30808, #35849, #2919 ) ;
#9343=CONICAL_SURFACE ( 'NONE', #30314, 4.000000000000000000, 1.047197551196595855 ) ;
#9457=ADVANCED_FACE ( 'NONE', ( #5940 ), #7477, .T. ) ;
#9475=FACE_OUTER_BOUND ( 'NONE', #24210, .T. ) ;
#9556=COLOUR_RGB ( '', 0.09019608, 0.27058824, 0.51372549) ;
#9594=CARTESIAN_POINT ( 'NONE',  ( 4.000000000000004441, -1.549102112939112486, -0.1578953385959447620 ) ) ;
#9609=DIRECTION ( 'NONE',  ( 0.000000000000000000, 0.000000000000000000, 1.000000000000000000 ) ) ;
#9626=CARTESIAN_POINT ( 'NONE',  ( -2.339468227445729021, -3.268109542640674547, -1.786138375875142494E-14 ) ) ;
#9644=CARTESIAN_POINT ( 'NONE',  ( 2.500000000000002220, 3.061616997868386099E-16, -5.574599999999999334 ) ) ;
#9767=CARTESIAN_POINT ( 'NONE',  ( 0.6543461111163461075, 4.241015250120812929, -5.460849780464856806 ) ) ;
#9796=DIRECTION ( 'NONE',  ( 0.000000000000000000, 0.000000000000000000, -1.000000000000000000 ) ) ;
#9813=DIRECTION ( 'NONE',  ( -0.8191520442889896891, 0.000000000000000000, -0.5735764363510490460 ) ) ;
#9873=DIRECTION ( 'NONE',  ( 1.000000000000000000, 0.000000000000000000, 0.000000000000000000 ) ) ;
#9944=VERTEX_POINT ( 'NONE', #4563 ) ;
#10181=EDGE_CURVE ( 'NONE', #47052, #478, #37690, .T. ) ;
#10203=CARTESIAN_POINT ( 'NONE',  ( -3.345653888883663996, 2.687187980154699840, -5.460849780464863024 ) ) ;
#10224=CARTESIAN_POINT ( 'NONE',  ( 1.660531772554325158, -3.660093687634888404, -5.599999999999981881 ) ) ;
#10241=FILL_AREA_STYLE ('',( #5205 ) ) ;
#10278=DIRECTION ( 'NONE',  ( -0.000000000000000000, -0.000000000000000000, 1.000000000000000000 ) ) ;
#10432=ORIENTED_EDGE ( 'NONE', *, *, #3372, .T. ) ;
#10469=CIRCLE ( 'NONE', #1449, 2.500000000000002220 ) ;
#10471=CARTESIAN_POINT ( 'NONE',  ( 0.3263565795980677420, -4.430380094434308802, -0.2484800633750392507 ) ) ;
#10534=EDGE_CURVE ( 'NONE', #18237, #32229, #20405, .T. ) ;
#10618=CIRCLE ( 'NONE', #8624, 4.000000000000000888 ) ;
#10670=CARTESIAN_POINT ( 'NONE',  ( 2.000000000000027089, 3.464101615137739731, 0.000000000000000000 ) ) ;
#10793=FACE_OUTER_BOUND ( 'NONE', #36130, .T. ) ;
#10935=PLANE ( 'NONE',  #20703 ) ;
#11200=EDGE_CURVE ( 'NONE', #1947, #14833, #27222, .T. ) ;
#11236=CARTESIAN_POINT ( 'NONE',  ( -4.000000000000000000, -0.3902508023145548899, -5.600000000000000533 ) ) ;
#11297=ORIENTED_EDGE ( 'NONE', *, *, #36344, .T. ) ;
#11349=VECTOR ( 'NONE', #57819, 1000.000000000000000 ) ;
#11354=ORIENTED_EDGE ( 'NONE', *, *, #16843, .F. ) ;
#11530=CARTESIAN_POINT ( 'NONE',  ( 0.000000000000000000, 0.000000000000000000, -5.600000000000000533 ) ) ;
#11607=DIRECTION ( 'NONE',  ( -1.000000000000000000, 0.000000000000000000, 0.000000000000000000 ) ) ;
#11608=DIRECTION ( 'NONE',  ( -0.000000000000000000, 0.000000000000000000, -1.000000000000000000 ) ) ;
#11742=DIRECTION ( 'NONE',  ( -0.8660254037844372643, -0.5000000000000024425, 0.000000000000000000 ) ) ;
#11843=FACE_BOUND ( 'NONE', #23192, .T. ) ;
#11961=DIRECTION ( 'NONE',  ( 0.000000000000000000, -0.000000000000000000, 1.000000000000000000 ) ) ;
#12355=EDGE_LOOP ( 'NONE', ( #23619, #5783, #18210, #61785 ) ) ;
#12362=AXIS2_PLACEMENT_3D ( 'NONE', #1062, #24577, #34916 ) ;
#12372=DIRECTION ( 'NONE',  ( -1.000000000000000000, 0.000000000000000000, 0.000000000000000000 ) ) ;
#12423=ORIENTED_EDGE ( 'NONE', *, *, #52292, .T. ) ;
#12448=CARTESIAN_POINT ( 'NONE',  ( 1.214306433183764966E-14, 4.618802153517020059, 0.000000000000000000 ) ) ;
#12575=EDGE_CURVE ( 'NONE', #38564, #21005, #37699, .T. ) ;
#12759=EDGE_LOOP ( 'NONE', ( #53486, #7234, #10432 ) ) ;
#12873=ORIENTED_EDGE ( 'NONE', *, *, #42077, .T. ) ;
#12915=( GEOMETRIC_REPRESENTATION_CONTEXT ( 3 ) GLOBAL_UNCERTAINTY_ASSIGNED_CONTEXT ( ( #2296 ) ) GLOBAL_UNIT_ASSIGNED_CONTEXT ( ( #22184, #36604, #50977 ) ) REPRESENTATION_CONTEXT ( 'NONE', 'WORKASPACE' ) );
#12924=CARTESIAN_POINT ( 'NONE',  ( 1.084202172485504434E-14, 4.618802153517020059, -0.3572655899081733644 ) ) ;
#12930=CARTESIAN_POINT ( 'NONE',  ( -2.500000000000002220, 3.061616997868386099E-16, -25.03750572909317285 ) ) ;
#12970=EDGE_CURVE ( 'NONE', #56562, #26742, #35759, .T. ) ;
#13034=CARTESIAN_POINT ( 'NONE',  ( 2.681483223904246760, -3.070647092368467668, -2.072929885643508434E-14 ) ) ;
#13067=ORIENTED_EDGE ( 'NONE', *, *, #56551, .F. ) ;
#13221=CARTESIAN_POINT ( 'NONE',  ( 1.318516776095788545, 3.857556137907071747, 2.454790609853964971E-15 ) ) ;
#13308=DIRECTION ( 'NONE',  ( -0.8191520442889896891, 1.003171929053522158E-16, 0.5735764363510490460 ) ) ;
#13332=CARTESIAN_POINT ( 'NONE',  ( 1.660531772554323604, -3.660093687634888848, -2.106514470958295182E-14 ) ) ;
#13344=ADVANCED_FACE ( 'NONE', ( #49053 ), #38665, .T. ) ;
#13523=ADVANCED_FACE ( 'NONE', ( #7204 ), #1588, .T. ) ;
#13551=CYLINDRICAL_SURFACE ( 'NONE', #15260, 2.500000000000002220 ) ;
#13606=EDGE_CURVE ( 'NONE', #47052, #41414, #10618, .T. ) ;
#13675=PRESENTATION_STYLE_ASSIGNMENT (( #7709 ) ) ;
#13719=CARTESIAN_POINT ( 'NONE',  ( 4.000000000000003553, 2.309401076758480720, -5.599999999999999645 ) ) ;
#13821=DIRECTION ( 'NONE',  ( 0.000000000000000000, 0.000000000000000000, 1.000000000000000000 ) ) ;
#13822=DIRECTION ( 'NONE',  ( 1.000000000000000000, 0.000000000000000000, 0.000000000000000000 ) ) ;
#13921=AXIS2_PLACEMENT_3D ( 'NONE', #2011, #22376, #45901 ) ;
#14053=CARTESIAN_POINT ( 'NONE',  ( 2.000000000000010658, -3.464101615137748169, -5.600000000000000533 ) ) ;
#14121=LINE ( 'NONE', #33222, #23868 ) ;
#14302=ORIENTED_EDGE ( 'NONE', *, *, #47729, .F. ) ;
#14366=DIRECTION ( 'NONE',  ( 1.000000000000000000, 0.000000000000000000, 0.000000000000000000 ) ) ;
#14443=CARTESIAN_POINT ( 'NONE',  ( 0.000000000000000000, 0.000000000000000000, -5.574599999999999334 ) ) ;
#14506=VERTEX_POINT ( 'NONE', #30105 ) ;
#14551=AXIS2_PLACEMENT_3D ( 'NONE', #41190, #55244, #12372 ) ;
#14677=AXIS2_PLACEMENT_3D ( 'NONE', #3759, #61387, #13822 ) ;
#14731=CARTESIAN_POINT ( 'NONE',  ( -4.000000000000000000, 0.7862748000878058141, -0.03447227762756577968 ) ) ;
#14740=DIRECTION ( 'NONE',  ( 0.5000000000000066613, 0.8660254037844348218, -0.000000000000000000 ) ) ;
#14833=VERTEX_POINT ( 'NONE', #57285 ) ;
#15260=AXIS2_PLACEMENT_3D ( 'NONE', #47364, #60828, #57050 ) ;
#15345=ORIENTED_EDGE ( 'NONE', *, *, #55929, .F. ) ;
#15398=DIRECTION ( 'NONE',  ( -0.000000000000000000, -0.000000000000000000, 1.000000000000000000 ) ) ;
#15440=CARTESIAN_POINT ( 'NONE',  ( -1.318516776095821186, -3.857556137907092175, -1.739862437281285109E-14 ) ) ;
#15564=STYLED_ITEM ( 'NONE', ( #13675 ), #7748 ) ;
#15582=ADVANCED_FACE ( 'NONE', ( #53075 ), #28162, .T. ) ;
#15591=APPLICATION_CONTEXT ( 'automotive_design' ) ;
#15711=CARTESIAN_POINT ( 'NONE',  ( -4.000000000000000000, 0.000000000000000000, -5.599999999999999645 ) ) ;
#15715=DIRECTION ( 'NONE',  ( 0.000000000000000000, 0.000000000000000000, 1.000000000000000000 ) ) ;
#15734=ORIENTED_EDGE ( 'NONE', *, *, #2128, .T. ) ;
#15743=CIRCLE ( 'NONE', #48773, 2.500000000000002220 ) ;
#15906=CARTESIAN_POINT ( 'NONE',  ( -3.673643420401911275, -2.497823135841290565, -5.351519936624989704 ) ) ;
#15939=DIRECTION ( 'NONE',  ( -1.000000000000000000, 0.000000000000000000, 0.000000000000000000 ) ) ;
#15944=CARTESIAN_POINT ( 'NONE',  ( -4.000000000000000000, -0.7779732554280797130, -5.566455648918322119 ) ) ;
#15954=B_SPLINE_CURVE_WITH_KNOTS ( 'NONE', 3,
 ( #54233, #58311, #15440, #1614 ),
 .UNSPECIFIED., .F., .F.,
 ( 4, 4 ),
 ( 2.380737582495642427E-07, 0.002336974151641604130 ),
 .UNSPECIFIED. ) ;
#15978=EDGE_CURVE ( 'NONE', #16995, #32229, #46706, .T. ) ;
#16075=FACE_OUTER_BOUND ( 'NONE', #53702, .T. ) ;
#16237=LINE ( 'NONE', #41834, #43578 ) ;
#16278=VERTEX_POINT ( 'NONE', #1445 ) ;
#16301=ORIENTED_EDGE ( 'NONE', *, *, #47729, .T. ) ;
#16313=CARTESIAN_POINT ( 'NONE',  ( 3.673643420401900173, 2.497823135841254150, -5.351519936625005691 ) ) ;
#16600=ORIENTED_EDGE ( 'NONE', *, *, #10181, .F. ) ;
#16612=ORIENTED_EDGE ( 'NONE', *, *, #51244, .T. ) ;
#16641=ADVANCED_FACE ( 'NONE', ( #33284 ), #13551, .F. ) ;
#16666=ORIENTED_EDGE ( 'NONE', *, *, #13606, .T. ) ;
#16680=ORIENTED_EDGE ( 'NONE', *, *, #19278, .F. ) ;
#16800=CARTESIAN_POINT ( 'NONE',  ( 3.345653888883671101, -2.687187980154741140, -0.1391502195351564664 ) ) ;
#16843=EDGE_CURVE ( 'NONE', #48540, #51786, #29526, .T. ) ;
#16866=CARTESIAN_POINT ( 'NONE',  ( 1.084202172485504434E-14, 4.618802153517020059, -0.3572655899081733644 ) ) ;
#16924=EDGE_CURVE ( 'NONE', #9944, #16995, #7214, .T. ) ;
#16995=VERTEX_POINT ( 'NONE', #29838 ) ;
#17039=ORIENTED_EDGE ( 'NONE', *, *, #46537, .T. ) ;
#17111=ORIENTED_EDGE ( 'NONE', *, *, #48509, .T. ) ;
#17131=ORIENTED_EDGE ( 'NONE', *, *, #15978, .F. ) ;
#17150=APPLICATION_CONTEXT ( 'automotive_design' ) ;
#17220=ORIENTED_EDGE ( 'NONE', *, *, #56869, .T. ) ;
#17373=EDGE_LOOP ( 'NONE', ( #15734, #44637, #42358, #11354 ) ) ;
#17379=CARTESIAN_POINT ( 'NONE',  ( -1.318516776095820742, -3.857556137907092619, -5.599999999999983658 ) ) ;
#17505=VERTEX_POINT ( 'NONE', #1479 ) ;
#17682=AXIS2_PLACEMENT_3D ( 'NONE', #28407, #23719, #38154 ) ;
#17826=CARTESIAN_POINT ( 'NONE',  ( -0.6554360035617894376, 4.240386000424038571, -5.441324518471509997 ) ) ;
#17890=CIRCLE ( 'NONE', #13921, 4.000000000000000888 ) ;
#17895=ORIENTED_EDGE ( 'NONE', *, *, #23062, .F. ) ;
#17960=CARTESIAN_POINT ( 'NONE',  ( 4.000000000000000000, 0.000000000000000000, -5.600000000000000533 ) ) ;
#17974=PRODUCT_DEFINITION_CONTEXT ( 'detailed design', #15591, 'design' ) ;
#17988=DIRECTION ( 'NONE',  ( -0.5000000000000024425, 0.8660254037844372643, 0.000000000000000000 ) ) ;
#18166=CARTESIAN_POINT ( 'NONE',  ( 0.000000000000000000, 0.000000000000000000, -0.2800830152838832965 ) ) ;
#18210=ORIENTED_EDGE ( 'NONE', *, *, #16843, .T. ) ;
#18223=ORIENTED_EDGE ( 'NONE', *, *, #41201, .T. ) ;
#18237=VERTEX_POINT ( 'NONE', #26318 ) ;
#18386=DIRECTION ( 'NONE',  ( -0.000000000000000000, 0.000000000000000000, -1.000000000000000000 ) ) ;
#18406=ORIENTED_EDGE ( 'NONE', *, *, #48030, .T. ) ;
#18438=EDGE_LOOP ( 'NONE', ( #41725, #51784, #34600 ) ) ;
#18440=CARTESIAN_POINT ( 'NONE',  ( -1.321505333908964186, 3.855830693249140850, -5.565789719053469753 ) ) ;
#18480=ORIENTED_EDGE ( 'NONE', *, *, #13606, .F. ) ;
#18503=DIRECTION ( 'NONE',  ( -1.000000000000000000, 0.000000000000000000, 0.000000000000000000 ) ) ;
#18901=PRODUCT_DEFINITION_FORMATION_WITH_SPECIFIED_SOURCE ( 'ANY', '', #34426, .NOT_KNOWN. ) ;
#18978=LINE ( 'NONE', #42174, #26867 ) ;
#19065=ORIENTED_EDGE ( 'NONE', *, *, #48344, .T. ) ;
#19074=FACE_OUTER_BOUND ( 'NONE', #27004, .T. ) ;
#19191=CARTESIAN_POINT ( 'NONE',  ( 2.000000000000027089, 3.464101615137739731, -5.600000000000000533 ) ) ;
#19222=FACE_OUTER_BOUND ( 'NONE', #18438, .T. ) ;
#19246=DIRECTION ( 'NONE',  ( -0.5000000000000055511, -0.8660254037844354880, 0.000000000000000000 ) ) ;
#19278=EDGE_CURVE ( 'NONE', #14506, #6786, #37603, .T. ) ;
#19338=LINE ( 'NONE', #13719, #39507 ) ;
#19367=CARTESIAN_POINT ( 'NONE',  ( 0.000000000000000000, 0.000000000000000000, -5.599999999999999645 ) ) ;
#19372=CARTESIAN_POINT ( 'NONE',  ( 2.500000000000002220, 0.000000000000000000, -25.03750572909317285 ) ) ;
#19436=CARTESIAN_POINT ( 'NONE',  ( 4.000000000000000000, 0.000000000000000000, 0.000000000000000000 ) ) ;
#19524=ORIENTED_EDGE ( 'NONE', *, *, #48923, .F. ) ;
#19527=AXIS2_PLACEMENT_3D ( 'NONE', #4909, #28118, #59076 ) ;
#19626=ADVANCED_FACE ( 'NONE', ( #32827 ), #33440, .F. ) ;
#19636=CARTESIAN_POINT ( 'NONE',  ( 4.000000000000003553, -0.3902508023145564442, -1.995609623731131599E-15 ) ) ;
#19638=EDGE_LOOP ( 'NONE', ( #17131, #44444, #9100 ) ) ;
#19650=SURFACE_SIDE_STYLE ('',( #9304 ) ) ;
#19746=ORIENTED_EDGE ( 'NONE', *, *, #11200, .T. ) ;
#19756=ORIENTED_EDGE ( 'NONE', *, *, #38988, .F. ) ;
#19911=ORIENTED_EDGE ( 'NONE', *, *, #7489, .F. ) ;
#19953=VERTEX_POINT ( 'NONE', #48832 ) ;
#20092=DIRECTION ( 'NONE',  ( 0.000000000000000000, 0.000000000000000000, -1.000000000000000000 ) ) ;
#20130=ORIENTED_EDGE ( 'NONE', *, *, #56551, .T. ) ;
#20405=LINE ( 'NONE', #58582, #29833 ) ;
#20418=ORIENTED_EDGE ( 'NONE', *, *, #21095, .F. ) ;
#20447=DIRECTION ( 'NONE',  ( -1.000000000000000000, 0.000000000000000000, 0.000000000000000000 ) ) ;
#20630=AXIS2_PLACEMENT_3D ( 'NONE', #6107, #25243, #38921 ) ;
#20703=AXIS2_PLACEMENT_3D ( 'NONE', #5573, #30019, #15939 ) ;
#20778=CARTESIAN_POINT ( 'NONE',  ( -2.000000000000009770, 3.464101615137749057, -5.600000000000000533 ) ) ;
#20889=DIRECTION ( 'NONE',  ( -0.000000000000000000, 0.000000000000000000, -1.000000000000000000 ) ) ;
#20937=DIRECTION ( 'NONE',  ( 1.000000000000000000, 0.000000000000000000, 0.000000000000000000 ) ) ;
#21005=VERTEX_POINT ( 'NONE', #52849 ) ;
#21021=CARTESIAN_POINT ( 'NONE',  ( 2.678494666091051801, 3.072372537026355044, -5.565789719053469753 ) ) ;
#21081=EDGE_CURVE ( 'NONE', #9944, #17505, #7456, .T. ) ;
#21095=EDGE_CURVE ( 'NONE', #30298, #3027, #27515, .T. ) ;
#21286=ORIENTED_EDGE ( 'NONE', *, *, #31052, .F. ) ;
#21389=ORIENTED_EDGE ( 'NONE', *, *, #31698, .F. ) ;
#21410=CARTESIAN_POINT ( 'NONE',  ( 3.999999999999990674, -2.309401076758548221, -5.242734410091827613 ) ) ;
#21449=DIRECTION ( 'NONE',  ( 0.000000000000000000, -0.000000000000000000, 1.000000000000000000 ) ) ;
#21548=CARTESIAN_POINT ( 'NONE',  ( -0.3263565795980851170, 4.430380094434251959, -0.2484800633750073040 ) ) ;
#21554=EDGE_LOOP ( 'NONE', ( #44587, #58128, #1798, #17895 ) ) ;
#21706=EDGE_CURVE ( 'NONE', #41414, #56562, #7269, .T. ) ;
#21820=ORIENTED_EDGE ( 'NONE', *, *, #28831, .F. ) ;
#21843=CARTESIAN_POINT ( 'NONE',  ( 0.000000000000000000, 0.000000000000000000, -5.294516984716111097 ) ) ;
#21919=AXIS2_PLACEMENT_3D ( 'NONE', #53115, #56886, #28091 ) ;
#22049=AXIS2_PLACEMENT_3D ( 'NONE', #22673, #17988, #11742 ) ;
#22184=( LENGTH_UNIT ( ) NAMED_UNIT ( * ) SI_UNIT ( .MILLI., .METRE. ) );
#22215=CARTESIAN_POINT ( 'NONE',  ( -1.660531772554312280, 3.660093687634848436, -5.600000000000003197 ) ) ;
#22250=B_SPLINE_CURVE_WITH_KNOTS ( 'NONE', 3,
 ( #45006, #49667, #46230, #59365, #54972, #6723 ),
 .UNSPECIFIED., .F., .F.,
 ( 4, 2, 4 ),
 ( 0.006456566858647394894, 0.007625406818786665576, 0.008794246778925936259 ),
 .UNSPECIFIED. ) ;
#22376=DIRECTION ( 'NONE',  ( -0.000000000000000000, 0.000000000000000000, -1.000000000000000000 ) ) ;
#22420=VERTEX_POINT ( 'NONE', #25977 ) ;
#22515=EDGE_CURVE ( 'NONE', #17505, #16995, #59874, .T. ) ;
#22614=FACE_OUTER_BOUND ( 'NONE', #42054, .T. ) ;
#22673=CARTESIAN_POINT ( 'NONE',  ( 1.155036213957052500E-14, 4.618802153517020059, -5.599999999999999645 ) ) ;
#22732=ORIENTED_EDGE ( 'NONE', *, *, #26251, .T. ) ;
#22855=DIRECTION ( 'NONE',  ( 1.000000000000000000, 0.000000000000000000, 0.000000000000000000 ) ) ;
#22887=CARTESIAN_POINT ( 'NONE',  ( 2.678494666091051357, 3.072372537026354156, -0.03421028094653023183 ) ) ;
#23023=CARTESIAN_POINT ( 'NONE',  ( -1.660531772554312280, 3.660093687634848436, 2.744386749103932310E-15 ) ) ;
#23060=CARTESIAN_POINT ( 'NONE',  ( -7.459310946700270506E-14, -4.618802153517020948, -5.242734410091827613 ) ) ;
#23062=EDGE_CURVE ( 'NONE', #19953, #38564, #58922, .T. ) ;
#23192=EDGE_LOOP ( 'NONE', ( #14302, #5554 ) ) ;
#23441=B_SPLINE_CURVE_WITH_KNOTS ( 'NONE', 3,
 ( #31228, #60035, #1465, #35024, #15906, #7395 ),
 .UNSPECIFIED., .F., .F.,
 ( 4, 2, 4 ),
 ( 0.002336974151641604130, 0.003500975885716476211, 0.004664977619791348291 ),
 .UNSPECIFIED. ) ;
#23484=EDGE_CURVE ( 'NONE', #1947, #331, #2154, .T. ) ;
#23619=ORIENTED_EDGE ( 'NONE', *, *, #55948, .F. ) ;
#23719=DIRECTION ( 'NONE',  ( -1.000000000000000000, 0.000000000000000000, 0.000000000000000000 ) ) ;
#23772=DIRECTION ( 'NONE',  ( 0.000000000000000000, 0.000000000000000000, 1.000000000000000000 ) ) ;
#23868=VECTOR ( 'NONE', #34455, 1000.000000000000000 ) ;
#24028=PRESENTATION_STYLE_ASSIGNMENT (( #509 ) ) ;
#24119=PLANE ( 'NONE',  #40979 ) ;
#24130=DIRECTION ( 'NONE',  ( -1.000000000000000000, 0.000000000000000000, 0.000000000000000000 ) ) ;
#24147=ORIENTED_EDGE ( 'NONE', *, *, #12575, .T. ) ;
#24200=CARTESIAN_POINT ( 'NONE',  ( 0.000000000000000000, 0.000000000000000000, -0.2800830152838832965 ) ) ;
#24205=CARTESIAN_POINT ( 'NONE',  ( 0.000000000000000000, 0.000000000000000000, -5.600000000000000533 ) ) ;
#24210=EDGE_LOOP ( 'NONE', ( #19065, #44534, #32440 ) ) ;
#24225=ORIENTED_EDGE ( 'NONE', *, *, #51244, .F. ) ;
#24259=DIRECTION ( 'NONE',  ( 1.000000000000000000, 0.000000000000000000, 0.000000000000000000 ) ) ;
#24317=CARTESIAN_POINT ( 'NONE',  ( 2.099999999999999645, 0.000000000000000000, -5.294516984716111097 ) ) ;
#24334=CARTESIAN_POINT ( 'NONE',  ( 0.000000000000000000, 0.000000000000000000, -5.294516984716111097 ) ) ;
#24577=DIRECTION ( 'NONE',  ( 0.000000000000000000, -0.000000000000000000, 1.000000000000000000 ) ) ;
#24648=( LENGTH_UNIT ( ) NAMED_UNIT ( * ) SI_UNIT ( .MILLI., .METRE. ) );
#24663=CARTESIAN_POINT ( 'NONE',  ( 0.000000000000000000, 0.000000000000000000, -5.599999999999999645 ) ) ;
#24910=CARTESIAN_POINT ( 'NONE',  ( -4.000000000000000000, 0.000000000000000000, 0.000000000000000000 ) ) ;
#25035=CARTESIAN_POINT ( 'NONE',  ( -2.681483223904239210, 3.070647092368425479, 2.604296331179000749E-15 ) ) ;
#25086=ORIENTED_EDGE ( 'NONE', *, *, #23062, .T. ) ;
#25199=CARTESIAN_POINT ( 'NONE',  ( -4.000000000000000000, -2.309401076758531346, -0.3572655899081733644 ) ) ;
#25243=DIRECTION ( 'NONE',  ( 0.000000000000000000, 0.000000000000000000, -1.000000000000000000 ) ) ;
#25536=ADVANCED_FACE ( 'NONE', ( #16075 ), #36075, .T. ) ;
#25564=MECHANICAL_DESIGN_GEOMETRIC_PRESENTATION_REPRESENTATION('',(#15564),#27534);
#25580=CARTESIAN_POINT ( 'NONE',  ( 0.000000000000000000, 0.000000000000000000, 0.000000000000000000 ) ) ;
#25590=ORIENTED_EDGE ( 'NONE', *, *, #46537, .F. ) ;
#25633=CARTESIAN_POINT ( 'NONE',  ( -4.000000000000000000, -1.549102112939103826, -5.442104661404060906 ) ) ;
#25717=CARTESIAN_POINT ( 'NONE',  ( 0.000000000000000000, 0.000000000000000000, -5.600000000000000533 ) ) ;
#25761=CARTESIAN_POINT ( 'NONE',  ( 0.000000000000000000, 0.000000000000000000, 0.000000000000000000 ) ) ;
#25905=COLOUR_RGB ( '', 0.09019608, 0.27058824, 0.51372549) ;
#25919=DIRECTION ( 'NONE',  ( 0.000000000000000000, 0.000000000000000000, -1.000000000000000000 ) ) ;
#25923=ORIENTED_EDGE ( 'NONE', *, *, #31698, .T. ) ;
#25977=CARTESIAN_POINT ( 'NONE',  ( -4.000000000000000000, -2.309401076758531346, -5.242734410091827613 ) ) ;
#26035=ADVANCED_FACE ( 'NONE', ( #49119 ), #53901, .T. ) ;
#26064=CARTESIAN_POINT ( 'NONE',  ( 4.000000000000000000, 0.000000000000000000, -5.600000000000000533 ) ) ;
#26213=PLANE ( 'NONE',  #26733 ) ;
#26225=CARTESIAN_POINT ( 'NONE',  ( 0.000000000000000000, 0.000000000000000000, 0.000000000000000000 ) ) ;
#26251=EDGE_CURVE ( 'NONE', #48322, #44297, #47943, .T. ) ;
#26318=CARTESIAN_POINT ( 'NONE',  ( -4.000000000000000000, 2.309401076758531346, -5.242734410091827613 ) ) ;
#26416=CARTESIAN_POINT ( 'NONE',  ( 0.000000000000000000, 0.000000000000000000, -5.599999999999999645 ) ) ;
#26444=FACE_OUTER_BOUND ( 'NONE', #19638, .T. ) ;
#26642=AXIS2_PLACEMENT_3D ( 'NONE', #56577, #18386, #51877 ) ;
#26733=AXIS2_PLACEMENT_3D ( 'NONE', #12448, #25919, #30921 ) ;
#26742=VERTEX_POINT ( 'NONE', #20778 ) ;
#26776=AXIS2_PLACEMENT_3D ( 'NONE', #34735, #30014, #55656 ) ;
#26832=( LENGTH_UNIT ( ) NAMED_UNIT ( * ) SI_UNIT ( .MILLI., .METRE. ) );
#26867=VECTOR ( 'NONE', #38094, 1000.000000000000000 ) ;
#26970=ORIENTED_EDGE ( 'NONE', *, *, #56869, .F. ) ;
#26997=CARTESIAN_POINT ( 'NONE',  ( 4.000000000000002665, 1.935983797701078313, -5.350530693383766412 ) ) ;
#27004=EDGE_LOOP ( 'NONE', ( #58816, #61326, #52240, #41868 ) ) ;
#27183=CARTESIAN_POINT ( 'NONE',  ( 3.999999999999990674, -2.309401076758548221, -0.3572655899081733644 ) ) ;
#27222=B_SPLINE_CURVE_WITH_KNOTS ( 'NONE', 3,
 ( #30873, #16800, #13034, #7999 ),
 .UNSPECIFIED., .F., .F.,
 ( 4, 4 ),
 ( 2.380737581781750353E-07, 0.002336974151641521731 ),
 .UNSPECIFIED. ) ;
#27300=CARTESIAN_POINT ( 'NONE',  ( 4.000000000000003553, 2.309401076758524685, -5.242734410091827613 ) ) ;
#27357=UNCERTAINTY_MEASURE_WITH_UNIT (LENGTH_MEASURE( 1.000000000000000082E-05 ), #24648, 'distance_accuracy_value', 'NONE');
#27365=PLANE ( 'NONE',  #22049 ) ;
#27384=EDGE_LOOP ( 'NONE', ( #45055, #54688, #43712, #35537, #19524, #5977 ) ) ;
#27407=VECTOR ( 'NONE', #13308, 1000.000000000000114 ) ;
#27515=CIRCLE ( 'NONE', #19527, 2.500000000000002220 ) ;
#27534=( GEOMETRIC_REPRESENTATION_CONTEXT ( 3 ) GLOBAL_UNCERTAINTY_ASSIGNED_CONTEXT ( ( #9165 ) ) GLOBAL_UNIT_ASSIGNED_CONTEXT ( ( #26832, #55942, #47188 ) ) REPRESENTATION_CONTEXT ( 'NONE', 'WORKASPACE' ) );
#27550=EDGE_LOOP ( 'NONE', ( #47058, #25086, #24147, #16301 ) ) ;
#27659=CARTESIAN_POINT ( 'NONE',  ( 2.060000000000000941, 0.000000000000000000, -0.3080913168122707546 ) ) ;
#27711=CARTESIAN_POINT ( 'NONE',  ( -1.321505333908964186, 3.855830693249140850, -0.03421028094653189716 ) ) ;
#27777=ORIENTED_EDGE ( 'NONE', *, *, #36344, .F. ) ;
#27909=ORIENTED_EDGE ( 'NONE', *, *, #45929, .F. ) ;
#28091=DIRECTION ( 'NONE',  ( -1.000000000000000000, 0.000000000000000000, 0.000000000000000000 ) ) ;
#28118=DIRECTION ( 'NONE',  ( 0.000000000000000000, -0.000000000000000000, 1.000000000000000000 ) ) ;
#28123=DIRECTION ( 'NONE',  ( -0.000000000000000000, -0.000000000000000000, 1.000000000000000000 ) ) ;
#28143=DIRECTION ( 'NONE',  ( -0.000000000000000000, -0.000000000000000000, 1.000000000000000000 ) ) ;
#28156=LINE ( 'NONE', #47587, #1615 ) ;
#28162=CONICAL_SURFACE ( 'NONE', #52164, 4.000000000000000000, 1.047197551196595855 ) ;
#28165=DIRECTION ( 'NONE',  ( 0.000000000000000000, 0.000000000000000000, -1.000000000000000000 ) ) ;
#28250=B_SPLINE_CURVE_WITH_KNOTS ( 'NONE', 3,
 ( #61077, #51991, #22887, #9083, #52604, #28810 ),
 .UNSPECIFIED., .F., .F.,
 ( 4, 2, 4 ),
 ( 0.002336974151641576809, 0.003500975885716453226, 0.004664977619791330077 ),
 .UNSPECIFIED. ) ;
#28268=ORIENTED_EDGE ( 'NONE', *, *, #35890, .F. ) ;
#28285=DIRECTION ( 'NONE',  ( 1.000000000000000000, 0.000000000000000000, 0.000000000000000000 ) ) ;
#28289=CIRCLE ( 'NONE', #3274, 4.000000000000000888 ) ;
#28407=CARTESIAN_POINT ( 'NONE',  ( 4.000000000000003553, 2.309401076758480720, -5.599999999999999645 ) ) ;
#28500=PLANE ( 'NONE',  #38561 ) ;
#28541=ORIENTED_EDGE ( 'NONE', *, *, #42518, .F. ) ;
#28810=CARTESIAN_POINT ( 'NONE',  ( 4.000000000000003553, 2.309401076758524685, -0.3572655899081733644 ) ) ;
#28831=EDGE_CURVE ( 'NONE', #16995, #29392, #60896, .T. ) ;
#28889=( GEOMETRIC_REPRESENTATION_CONTEXT ( 3 ) GLOBAL_UNCERTAINTY_ASSIGNED_CONTEXT ( ( #27357 ) ) GLOBAL_UNIT_ASSIGNED_CONTEXT ( ( #24648, #52837, #48443 ) ) REPRESENTATION_CONTEXT ( 'NONE', 'WORKASPACE' ) );
#28962=CARTESIAN_POINT ( 'NONE',  ( 0.000000000000000000, 0.000000000000000000, -25.03750572909317285 ) ) ;
#29054=FACE_OUTER_BOUND ( 'NONE', #21554, .T. ) ;
#29225=AXIS2_PLACEMENT_3D ( 'NONE', #28962, #48077, #24259 ) ;
#29299=CARTESIAN_POINT ( 'NONE',  ( -2.681483223904233881, 3.070647092368428588, -5.600000000000003197 ) ) ;
#29318=CARTESIAN_POINT ( 'NONE',  ( 2.000000000000010658, -3.464101615137748169, -5.600000000000000533 ) ) ;
#29392=VERTEX_POINT ( 'NONE', #46851 ) ;
#29504=CONICAL_SURFACE ( 'NONE', #14551, 4.000000000000000000, 1.047197551196595855 ) ;
#29526=LINE ( 'NONE', #47418, #39273 ) ;
#29529=EDGE_LOOP ( 'NONE', ( #25590, #50282, #18406, #48207 ) ) ;
#29833=VECTOR ( 'NONE', #15715, 1000.000000000000000 ) ;
#29838=CARTESIAN_POINT ( 'NONE',  ( -4.000000000000000000, 0.000000000000000000, 0.000000000000000000 ) ) ;
#29873=CARTESIAN_POINT ( 'NONE',  ( -7.632783294297951215E-14, -4.618802153517020948, -0.3572655899081733644 ) ) ;
#30014=DIRECTION ( 'NONE',  ( -0.000000000000000000, -0.000000000000000000, 1.000000000000000000 ) ) ;
#30019=DIRECTION ( 'NONE',  ( 0.000000000000000000, 0.000000000000000000, -1.000000000000000000 ) ) ;
#30022=CARTESIAN_POINT ( 'NONE',  ( -4.000000000000000000, -2.309401076758531346, -5.242734410091827613 ) ) ;
#30105=CARTESIAN_POINT ( 'NONE',  ( 1.084202172485504434E-14, 4.618802153517020059, -5.242734410091827613 ) ) ;
#30156=ORIENTED_EDGE ( 'NONE', *, *, #8391, .T. ) ;
#30197=DIRECTION ( 'NONE',  ( -0.000000000000000000, -0.000000000000000000, 1.000000000000000000 ) ) ;
#30221=CARTESIAN_POINT ( 'NONE',  ( 3.999999999999990674, -2.309401076758548221, -5.242734410091827613 ) ) ;
#30250=DIRECTION ( 'NONE',  ( -0.000000000000000000, -0.000000000000000000, 1.000000000000000000 ) ) ;
#30298=VERTEX_POINT ( 'NONE', #30642 ) ;
#30314=AXIS2_PLACEMENT_3D ( 'NONE', #39307, #48377, #58365 ) ;
#30327=CARTESIAN_POINT ( 'NONE',  ( -4.000000000000000000, -1.933795701539610334, -5.351162342337702604 ) ) ;
#30445=ADVANCED_FACE ( 'NONE', ( #41316 ), #52759, .F. ) ;
#30465=DIRECTION ( 'NONE',  ( 0.000000000000000000, 0.000000000000000000, 1.000000000000000000 ) ) ;
#30571=EDGE_CURVE ( 'NONE', #46482, #41414, #47027, .T. ) ;
#30642=CARTESIAN_POINT ( 'NONE',  ( 2.500000000000002220, 0.000000000000000000, -5.600000000000000533 ) ) ;
#30717=DIRECTION ( 'NONE',  ( -0.000000000000000000, -0.000000000000000000, 1.000000000000000000 ) ) ;
#30743=AXIS2_PLACEMENT_3D ( 'NONE', #24663, #34088, #56930 ) ;
#30808=CARTESIAN_POINT ( 'NONE',  ( 0.000000000000000000, 0.000000000000000000, -5.600000000000000533 ) ) ;
#30873=CARTESIAN_POINT ( 'NONE',  ( 3.999999999999990674, -2.309401076758548221, -0.3572655899081733644 ) ) ;
#30921=DIRECTION ( 'NONE',  ( -1.000000000000000000, 0.000000000000000000, 0.000000000000000000 ) ) ;
#31052=EDGE_CURVE ( 'NONE', #51504, #40436, #28250, .T. ) ;
#31203=B_SPLINE_CURVE_WITH_KNOTS ( 'NONE', 3,
 ( #32546, #22215, #18440, #17826, #37252, #50697 ),
 .UNSPECIFIED., .F., .F.,
 ( 4, 2, 4 ),
 ( 0.002336974151641539946, 0.003500975885716448889, 0.004664977619791357832 ),
 .UNSPECIFIED. ) ;
#31228=CARTESIAN_POINT ( 'NONE',  ( -2.000000000000022649, -3.464101615137742396, -5.600000000000000533 ) ) ;
#31246=ORIENTED_EDGE ( 'NONE', *, *, #32906, .F. ) ;
#31332=ADVANCED_FACE ( 'NONE', ( #52225 ), #8289, .T. ) ;
#31432=DIRECTION ( 'NONE',  ( 0.000000000000000000, -0.000000000000000000, 1.000000000000000000 ) ) ;
#31495=SHAPE_DEFINITION_REPRESENTATION ( #46321, #53251 ) ;
#31698=EDGE_CURVE ( 'NONE', #331, #14833, #28289, .T. ) ;
#31866=CARTESIAN_POINT ( 'NONE',  ( 4.000000000000000000, 0.000000000000000000, 0.000000000000000000 ) ) ;
#31989=CARTESIAN_POINT ( 'NONE',  ( 0.000000000000000000, 0.000000000000000000, -5.599999999999999645 ) ) ;
#32014=CARTESIAN_POINT ( 'NONE',  ( 4.000000000000000000, 0.000000000000000000, -5.600000000000000533 ) ) ;
#32020=CARTESIAN_POINT ( 'NONE',  ( 2.000000000000027089, 3.464101615137739731, 0.000000000000000000 ) ) ;
#32068=EDGE_LOOP ( 'NONE', ( #16612, #40067, #53412 ) ) ;
#32188=ORIENTED_EDGE ( 'NONE', *, *, #19278, .T. ) ;
#32229=VERTEX_POINT ( 'NONE', #36063 ) ;
#32344=VECTOR ( 'NONE', #50908, 1000.000000000000000 ) ;
#32412=CARTESIAN_POINT ( 'NONE',  ( -2.060000000000000941, 2.522772406243548923E-16, -0.3080913168122707546 ) ) ;
#32440=ORIENTED_EDGE ( 'NONE', *, *, #21706, .T. ) ;
#32503=EDGE_LOOP ( 'NONE', ( #2681, #17111, #22732 ) ) ;
#32546=CARTESIAN_POINT ( 'NONE',  ( -2.000000000000009770, 3.464101615137749057, -5.600000000000000533 ) ) ;
#32567=ORIENTED_EDGE ( 'NONE', *, *, #30571, .F. ) ;
#32779=CONICAL_SURFACE ( 'NONE', #5719, 2.060000000000000941, 0.9599310885968777018 ) ;
#32827=FACE_OUTER_BOUND ( 'NONE', #42252, .T. ) ;
#32843=CARTESIAN_POINT ( 'NONE',  ( -3.673643420401911275, -2.497823135841289677, -0.2484800633750114396 ) ) ;
#32906=EDGE_CURVE ( 'NONE', #22420, #17505, #503, .T. ) ;
#32916=CIRCLE ( 'NONE', #44915, 4.000000000000000888 ) ;
#32925=FACE_OUTER_BOUND ( 'NONE', #27384, .T. ) ;
#32992=ORIENTED_EDGE ( 'NONE', *, *, #9231, .F. ) ;
#33004=CARTESIAN_POINT ( 'NONE',  ( 0.000000000000000000, 0.000000000000000000, -5.600000000000000533 ) ) ;
#33150=CARTESIAN_POINT ( 'NONE',  ( 0.000000000000000000, 0.000000000000000000, -5.600000000000000533 ) ) ;
#33222=CARTESIAN_POINT ( 'NONE',  ( 4.000000000000003553, -2.309401076758539784, -5.599999999999999645 ) ) ;
#33281=ADVANCED_BREP_SHAPE_REPRESENTATION ( '', ( #7748, #14677 ), #12915 ) ;
#33284=FACE_OUTER_BOUND ( 'NONE', #34073, .T. ) ;
#33440=PLANE ( 'NONE',  #17682 ) ;
#33693=CARTESIAN_POINT ( 'NONE',  ( 0.000000000000000000, 0.000000000000000000, -5.600000000000000533 ) ) ;
#34073=EDGE_LOOP ( 'NONE', ( #32992, #20418, #38481, #39449 ) ) ;
#34088=DIRECTION ( 'NONE',  ( 0.000000000000000000, 0.000000000000000000, 1.000000000000000000 ) ) ;
#34143=CARTESIAN_POINT ( 'NONE',  ( -2.500000000000002220, 3.061616997868386099E-16, -5.600000000000000533 ) ) ;
#34426=PRODUCT ( 'hex nut gradec_iso_ISO - 4034 - M5 - N', 'hex nut gradec_iso_ISO - 4034 - M5 - N', '', ( #3276 ) ) ;
#34455=DIRECTION ( 'NONE',  ( 0.000000000000000000, 0.000000000000000000, 1.000000000000000000 ) ) ;
#34502=DIRECTION ( 'NONE',  ( 1.000000000000000000, 0.000000000000000000, 0.000000000000000000 ) ) ;
#34591=CARTESIAN_POINT ( 'NONE',  ( 0.6554360035617794455, -4.240386000424091861, -0.1586754815285204845 ) ) ;
#34600=ORIENTED_EDGE ( 'NONE', *, *, #12970, .T. ) ;
#34692=ORIENTED_EDGE ( 'NONE', *, *, #16924, .F. ) ;
#34735=CARTESIAN_POINT ( 'NONE',  ( 0.000000000000000000, 0.000000000000000000, 3.469446951953614189E-15 ) ) ;
#34891=DIRECTION ( 'NONE',  ( 1.000000000000000000, 0.000000000000000000, 0.000000000000000000 ) ) ;
#34916=DIRECTION ( 'NONE',  ( -1.000000000000000000, 8.881784197001252323E-16, 0.000000000000000000 ) ) ;
#34926=CARTESIAN_POINT ( 'NONE',  ( 0.000000000000000000, 0.000000000000000000, -0.3080913168122707546 ) ) ;
#35024=CARTESIAN_POINT ( 'NONE',  ( -3.344563996438217224, -2.687817229851499068, -5.441324518471498450 ) ) ;
#35134=DIRECTION ( 'NONE',  ( -1.000000000000000000, 1.776356839400250465E-15, 0.000000000000000000 ) ) ;
#35180=DIRECTION ( 'NONE',  ( -0.000000000000000000, 0.000000000000000000, -1.000000000000000000 ) ) ;
#35350=DIRECTION ( 'NONE',  ( -0.000000000000000000, -0.000000000000000000, 1.000000000000000000 ) ) ;
#35537=ORIENTED_EDGE ( 'NONE', *, *, #10534, .F. ) ;
#35541=B_SPLINE_CURVE_WITH_KNOTS ( 'NONE', 3,
 ( #32014, #41126, #55175, #7880, #26997, #27300 ),
 .UNSPECIFIED., .F., .F.,
 ( 4, 2, 4 ),
 ( 0.006456566858647417445, 0.007625406818786684658, 0.008794246778925951871 ),
 .UNSPECIFIED. ) ;
#35757=EDGE_LOOP ( 'NONE', ( #21820, #34692, #28541, #21389, #12873, #8801 ) ) ;
#35759=CIRCLE ( 'NONE', #43775, 4.000000000000000888 ) ;
#35849=DIRECTION ( 'NONE',  ( -0.000000000000000000, -0.000000000000000000, 1.000000000000000000 ) ) ;
#35890=EDGE_CURVE ( 'NONE', #6786, #51504, #6602, .T. ) ;
#35892=STYLED_ITEM ( 'NONE', ( #24028 ), #33281 ) ;
#35937=ADVANCED_FACE ( 'NONE', ( #22614 ), #36420, .T. ) ;
#35980=DIRECTION ( 'NONE',  ( 0.8191520442889896891, 1.003171929053522158E-16, -0.5735764363510490460 ) ) ;
#36036=ORIENTED_EDGE ( 'NONE', *, *, #42077, .F. ) ;
#36050=CARTESIAN_POINT ( 'NONE',  ( 0.000000000000000000, 0.000000000000000000, 0.000000000000000000 ) ) ;
#36063=CARTESIAN_POINT ( 'NONE',  ( -4.000000000000000000, 2.309401076758496263, -0.3572655899081631503 ) ) ;
#36075=CONICAL_SURFACE ( 'NONE', #5032, 4.000000000000000000, 1.047197551196595855 ) ;
#36091=ADVANCED_FACE ( 'NONE', ( #1556 ), #39680, .F. ) ;
#36130=EDGE_LOOP ( 'NONE', ( #36036, #58021, #21286 ) ) ;
#36344=EDGE_CURVE ( 'NONE', #478, #56169, #28156, .T. ) ;
#36357=ORIENTED_EDGE ( 'NONE', *, *, #55929, .T. ) ;
#36420=PLANE ( 'NONE',  #42807 ) ;
#36424=LINE ( 'NONE', #12930, #8466 ) ;
#36592=AXIS2_PLACEMENT_3D ( 'NONE', #33004, #52077, #47395 ) ;
#36604=( NAMED_UNIT ( * ) PLANE_ANGLE_UNIT ( ) SI_UNIT ( $, .RADIAN. ) );
#36650=AXIS2_PLACEMENT_3D ( 'NONE', #25717, #30717, #6257 ) ;
#36723=CIRCLE ( 'NONE', #44727, 2.500000000000000444 ) ;
#36731=CIRCLE ( 'NONE', #44733, 2.099999999999999645 ) ;
#37119=ORIENTED_EDGE ( 'NONE', *, *, #40023, .T. ) ;
#37124=ORIENTED_EDGE ( 'NONE', *, *, #49370, .T. ) ;
#37221=CARTESIAN_POINT ( 'NONE',  ( 2.000000000000027089, 3.464101615137739731, -5.600000000000000533 ) ) ;
#37252=CARTESIAN_POINT ( 'NONE',  ( -0.3263565795980851170, 4.430380094434251959, -5.351519936624993257 ) ) ;
#37309=DIRECTION ( 'NONE',  ( -1.000000000000000000, -3.552713678800500929E-15, 0.000000000000000000 ) ) ;
#37341=ORIENTED_EDGE ( 'NONE', *, *, #21081, .F. ) ;
#37351=ADVANCED_FACE ( 'NONE', ( #53801, #54111 ), #10935, .T. ) ;
#37422=EDGE_CURVE ( 'NONE', #16278, #21005, #36723, .T. ) ;
#37537=AXIS2_PLACEMENT_3D ( 'NONE', #1253, #20092, #6873 ) ;
#37579=CARTESIAN_POINT ( 'NONE',  ( -2.500000000000002220, 0.000000000000000000, -5.574599999999999334 ) ) ;
#37603=LINE ( 'NONE', #41686, #60807 ) ;
#37690=B_SPLINE_CURVE_WITH_KNOTS ( 'NONE', 3,
 ( #29318, #10224, #48737, #5490, #58421, #60825 ),
 .UNSPECIFIED., .F., .F.,
 ( 4, 2, 4 ),
 ( 0.002336974151641520864, 0.003500975885716454961, 0.004664977619791389057 ),
 .UNSPECIFIED. ) ;
#37699=LINE ( 'NONE', #27659, #41754 ) ;
#37753=DIRECTION ( 'NONE',  ( 0.8660254037844354880, -0.5000000000000055511, 0.000000000000000000 ) ) ;
#38094=DIRECTION ( 'NONE',  ( 0.000000000000000000, 0.000000000000000000, 1.000000000000000000 ) ) ;
#38154=DIRECTION ( 'NONE',  ( 0.000000000000000000, 0.000000000000000000, 1.000000000000000000 ) ) ;
#38362=CARTESIAN_POINT ( 'NONE',  ( -4.000000000000000000, -2.309401076758525573, -5.599999999999999645 ) ) ;
#38477=AXIS2_PLACEMENT_3D ( 'NONE', #14443, #51705, #24130 ) ;
#38481=ORIENTED_EDGE ( 'NONE', *, *, #38786, .T. ) ;
#38486=DIRECTION ( 'NONE',  ( 0.000000000000000000, 0.000000000000000000, 1.000000000000000000 ) ) ;
#38546=CARTESIAN_POINT ( 'NONE',  ( -4.000000000000000000, 0.000000000000000000, 0.000000000000000000 ) ) ;
#38553=CARTESIAN_POINT ( 'NONE',  ( 4.000000000000003553, 2.309401076758480720, -5.599999999999999645 ) ) ;
#38556=AXIS2_PLACEMENT_3D ( 'NONE', #19367, #38486, #14366 ) ;
#38561=AXIS2_PLACEMENT_3D ( 'NONE', #38553, #14740, #5907 ) ;
#38564=VERTEX_POINT ( 'NONE', #3088 ) ;
#38665=CONICAL_SURFACE ( 'NONE', #20630, 4.000000000000000000, 1.047197551196595855 ) ;
#38764=CARTESIAN_POINT ( 'NONE',  ( -4.000000000000000000, -2.309401076758525573, -5.599999999999999645 ) ) ;
#38786=EDGE_CURVE ( 'NONE', #30298, #7613, #56022, .T. ) ;
#38869=FACE_OUTER_BOUND ( 'NONE', #50396, .T. ) ;
#38921=DIRECTION ( 'NONE',  ( -1.000000000000000000, 0.000000000000000000, 0.000000000000000000 ) ) ;
#38966=DIRECTION ( 'NONE',  ( 1.000000000000000000, 0.000000000000000000, 0.000000000000000000 ) ) ;
#38988=EDGE_CURVE ( 'NONE', #44297, #22420, #23441, .T. ) ;
#39273=VECTOR ( 'NONE', #9813, 1000.000000000000114 ) ;
#39307=CARTESIAN_POINT ( 'NONE',  ( 0.000000000000000000, 0.000000000000000000, 0.000000000000000000 ) ) ;
#39336=CARTESIAN_POINT ( 'NONE',  ( 1.084202172485504434E-14, 4.618802153517020059, -0.3572655899081733644 ) ) ;
#39367=CARTESIAN_POINT ( 'NONE',  ( 4.000000000000003553, -1.933795701539622103, -0.2488376576623028413 ) ) ;
#39403=ADVANCED_FACE ( 'NONE', ( #44825 ), #32779, .F. ) ;
#39449=ORIENTED_EDGE ( 'NONE', *, *, #52731, .T. ) ;
#39507=VECTOR ( 'NONE', #9609, 1000.000000000000000 ) ;
#39680=CONICAL_SURFACE ( 'NONE', #7616, 2.500000000000002220, 0.9599310885968777018 ) ;
#39886=ORIENTED_EDGE ( 'NONE', *, *, #54788, .F. ) ;
#39907=CONICAL_SURFACE ( 'NONE', #61849, 4.000000000000000000, 1.047197551196595855 ) ;
#39965=AXIS2_PLACEMENT_3D ( 'NONE', #11530, #35350, #1181 ) ;
#40023=EDGE_CURVE ( 'NONE', #29392, #51504, #58631, .T. ) ;
#40067=ORIENTED_EDGE ( 'NONE', *, *, #50212, .T. ) ;
#40144=CARTESIAN_POINT ( 'NONE',  ( 0.000000000000000000, 0.000000000000000000, -5.574599999999999334 ) ) ;
#40162=CARTESIAN_POINT ( 'NONE',  ( 3.344563996438205677, 2.687817229851463097, -5.441324518471517102 ) ) ;
#40227=CARTESIAN_POINT ( 'NONE',  ( 0.000000000000000000, 0.000000000000000000, -5.574599999999999334 ) ) ;
#40436=VERTEX_POINT ( 'NONE', #47740 ) ;
#40526=DIRECTION ( 'NONE',  ( -0.000000000000000000, -0.000000000000000000, 1.000000000000000000 ) ) ;
#40552=DIRECTION ( 'NONE',  ( -1.000000000000000000, 0.000000000000000000, 0.000000000000000000 ) ) ;
#40816=ORIENTED_EDGE ( 'NONE', *, *, #55075, .F. ) ;
#40827=CARTESIAN_POINT ( 'NONE',  ( 0.6543461111163461075, 4.241015250120812929, -0.1391502195351438376 ) ) ;
#40894=CARTESIAN_POINT ( 'NONE',  ( 4.000000000000003553, 2.309401076758524685, -5.242734410091827613 ) ) ;
#40979=AXIS2_PLACEMENT_3D ( 'NONE', #52000, #18503, #13821 ) ;
#41126=CARTESIAN_POINT ( 'NONE',  ( 4.000000000000003553, 0.3904826640788068293, -5.599999999999999645 ) ) ;
#41190=CARTESIAN_POINT ( 'NONE',  ( 0.000000000000000000, 0.000000000000000000, 0.000000000000000000 ) ) ;
#41201=EDGE_CURVE ( 'NONE', #38564, #19953, #36731, .T. ) ;
#41263=SURFACE_STYLE_FILL_AREA ( #46571 ) ;
#41316=FACE_OUTER_BOUND ( 'NONE', #29529, .T. ) ;
#41376=ORIENTED_EDGE ( 'NONE', *, *, #23484, .T. ) ;
#41414=VERTEX_POINT ( 'NONE', #26064 ) ;
#41686=CARTESIAN_POINT ( 'NONE',  ( 1.155036213957052500E-14, 4.618802153517020059, -5.599999999999999645 ) ) ;
#41725=ORIENTED_EDGE ( 'NONE', *, *, #7489, .T. ) ;
#41754=VECTOR ( 'NONE', #52683, 1000.000000000000114 ) ;
#41781=CARTESIAN_POINT ( 'NONE',  ( 4.000000000000003553, -0.3902508023145557225, -5.599999999999998757 ) ) ;
#41834=CARTESIAN_POINT ( 'NONE',  ( 2.500000000000002220, 3.061616997868386099E-16, -5.574599999999999334 ) ) ;
#41868=ORIENTED_EDGE ( 'NONE', *, *, #49935, .F. ) ;
#42054=EDGE_LOOP ( 'NONE', ( #8202, #19746, #17220, #27777, #16600, #60338 ) ) ;
#42077=EDGE_CURVE ( 'NONE', #331, #51504, #59777, .T. ) ;
#42174=CARTESIAN_POINT ( 'NONE',  ( -2.099999999999999645, 2.571758278209440971E-16, -5.599999999999999645 ) ) ;
#42252=EDGE_LOOP ( 'NONE', ( #3547, #53673, #44823, #30156, #20130, #39886 ) ) ;
#42304=ADVANCED_FACE ( 'NONE', ( #11843, #45655 ), #26213, .F. ) ;
#42326=DIRECTION ( 'NONE',  ( 0.000000000000000000, -0.000000000000000000, 1.000000000000000000 ) ) ;
#42358=ORIENTED_EDGE ( 'NONE', *, *, #48030, .F. ) ;
#42518=EDGE_CURVE ( 'NONE', #14833, #9944, #17890, .T. ) ;
#42582=CONICAL_SURFACE ( 'NONE', #36592, 4.000000000000000000, 1.047197551196595855 ) ;
#42713=EDGE_LOOP ( 'NONE', ( #41376, #25923, #52180 ) ) ;
#42731=DIRECTION ( 'NONE',  ( -0.000000000000000000, -0.000000000000000000, 1.000000000000000000 ) ) ;
#42805=AXIS2_PLACEMENT_3D ( 'NONE', #40227, #40526, #34891 ) ;
#42807=AXIS2_PLACEMENT_3D ( 'NONE', #60805, #3178, #51401 ) ;
#42892=DIRECTION ( 'NONE',  ( 1.000000000000000000, 0.000000000000000000, 0.000000000000000000 ) ) ;
#43080=ADVANCED_FACE ( 'NONE', ( #55337 ), #39907, .T. ) ;
#43172=AXIS2_PLACEMENT_3D ( 'NONE', #24334, #30250, #48149 ) ;
#43177=CARTESIAN_POINT ( 'NONE',  ( 2.681483223904247648, -3.070647092368467224, -5.599999999999980105 ) ) ;
#43238=B_SPLINE_CURVE_WITH_KNOTS ( 'NONE', 3,
 ( #30022, #30327, #25633, #15944, #11236, #49437 ),
 .UNSPECIFIED., .F., .F.,
 ( 4, 2, 4 ),
 ( 0.004120275011746843581, 0.005288420935197119671, 0.006456566858647394894 ),
 .UNSPECIFIED. ) ;
#43467=ADVANCED_FACE ( 'NONE', ( #52419 ), #52114, .T. ) ;
#43578=VECTOR ( 'NONE', #35980, 1000.000000000000114 ) ;
#43623=CARTESIAN_POINT ( 'NONE',  ( 1.084202172485504434E-14, 4.618802153517020059, -5.242734410091827613 ) ) ;
#43668=CARTESIAN_POINT ( 'NONE',  ( 0.000000000000000000, 0.000000000000000000, -0.3080913168122707546 ) ) ;
#43712=ORIENTED_EDGE ( 'NONE', *, *, #15978, .T. ) ;
#43775=AXIS2_PLACEMENT_3D ( 'NONE', #31989, #42326, #37309 ) ;
#44132=ORIENTED_EDGE ( 'NONE', *, *, #35890, .T. ) ;
#44217=EDGE_LOOP ( 'NONE', ( #57138, #2845, #37341 ) ) ;
#44297=VERTEX_POINT ( 'NONE', #54381 ) ;
#44397=CIRCLE ( 'NONE', #12362, 4.000000000000000888 ) ;
#44444=ORIENTED_EDGE ( 'NONE', *, *, #28831, .T. ) ;
#44534=ORIENTED_EDGE ( 'NONE', *, *, #8391, .F. ) ;
#44587=ORIENTED_EDGE ( 'NONE', *, *, #3237, .F. ) ;
#44637=ORIENTED_EDGE ( 'NONE', *, *, #55948, .T. ) ;
#44727=AXIS2_PLACEMENT_3D ( 'NONE', #53500, #53202, #20937 ) ;
#44733=AXIS2_PLACEMENT_3D ( 'NONE', #24200, #9796, #28285 ) ;
#44783=CARTESIAN_POINT ( 'NONE',  ( -3.345653888883671989, 2.687187980154694511, -0.1391502195351393412 ) ) ;
#44823=ORIENTED_EDGE ( 'NONE', *, *, #30571, .T. ) ;
#44825=FACE_OUTER_BOUND ( 'NONE', #27550, .T. ) ;
#44851=CARTESIAN_POINT ( 'NONE',  ( 2.339468227445713921, 3.268109542640642573, -5.600000000000002309 ) ) ;
#44915=AXIS2_PLACEMENT_3D ( 'NONE', #26416, #31432, #40552 ) ;
#45006=CARTESIAN_POINT ( 'NONE',  ( -4.000000000000000000, 0.000000000000000000, -5.599999999999999645 ) ) ;
#45055=ORIENTED_EDGE ( 'NONE', *, *, #32906, .T. ) ;
#45063=B_SPLINE_CURVE_WITH_KNOTS ( 'NONE', 3,
 ( #45587, #60574, #17379, #7970 ),
 .UNSPECIFIED., .F., .F.,
 ( 4, 4 ),
 ( 2.380737582480036903E-07, 0.002336974151641604130 ),
 .UNSPECIFIED. ) ;
#45107=CARTESIAN_POINT ( 'NONE',  ( -4.000000000000000000, 1.935983797701054998, -0.2494693066162268769 ) ) ;
#45587=CARTESIAN_POINT ( 'NONE',  ( -7.459310946700270506E-14, -4.618802153517020948, -5.242734410091827613 ) ) ;
#45655=FACE_OUTER_BOUND ( 'NONE', #35757, .T. ) ;
#45901=DIRECTION ( 'NONE',  ( -1.000000000000000000, 0.000000000000000000, 0.000000000000000000 ) ) ;
#45929=EDGE_CURVE ( 'NONE', #56169, #9944, #15954, .T. ) ;
#46230=CARTESIAN_POINT ( 'NONE',  ( -4.000000000000000000, 0.7862748000878172494, -5.565527722372433317 ) ) ;
#46321=PRODUCT_DEFINITION_SHAPE ( 'NONE', 'NONE',  #8814 ) ;
#46482=VERTEX_POINT ( 'NONE', #30221 ) ;
#46537=EDGE_CURVE ( 'NONE', #3027, #30298, #15743, .T. ) ;
#46571=FILL_AREA_STYLE ('',( #51860 ) ) ;
#46706=B_SPLINE_CURVE_WITH_KNOTS ( 'NONE', 3,
 ( #38546, #57598, #14731, #7776, #45107, #50684 ),
 .UNSPECIFIED., .F., .F.,
 ( 4, 2, 4 ),
 ( 0.006456566858647395761, 0.007625406818786647362, 0.008794246778925899830 ),
 .UNSPECIFIED. ) ;
#46851=CARTESIAN_POINT ( 'NONE',  ( -2.000000000000009770, 3.464101615137749057, 0.000000000000000000 ) ) ;
#47027=B_SPLINE_CURVE_WITH_KNOTS ( 'NONE', 3,
 ( #21410, #56145, #7925, #59610, #41781, #17960 ),
 .UNSPECIFIED., .F., .F.,
 ( 4, 2, 4 ),
 ( 0.004120275011746849653, 0.005288420935197133549, 0.006456566858647417445 ),
 .UNSPECIFIED. ) ;
#47052=VERTEX_POINT ( 'NONE', #52027 ) ;
#47058=ORIENTED_EDGE ( 'NONE', *, *, #52292, .F. ) ;
#47188=( NAMED_UNIT ( * ) SI_UNIT ( $, .STERADIAN. ) SOLID_ANGLE_UNIT ( ) );
#47208=ADVANCED_FACE ( 'NONE', ( #29054 ), #53156, .F. ) ;
#47231=EDGE_CURVE ( 'NONE', #46482, #47052, #56854, .T. ) ;
#47242=DIRECTION ( 'NONE',  ( 1.000000000000000000, 0.000000000000000000, 0.000000000000000000 ) ) ;
#47364=CARTESIAN_POINT ( 'NONE',  ( 0.000000000000000000, 0.000000000000000000, -25.03750572909317285 ) ) ;
#47395=DIRECTION ( 'NONE',  ( 1.000000000000000000, 0.000000000000000000, 0.000000000000000000 ) ) ;
#47418=CARTESIAN_POINT ( 'NONE',  ( -2.500000000000002220, 0.000000000000000000, -5.574599999999999334 ) ) ;
#47566=CYLINDRICAL_SURFACE ( 'NONE', #38556, 2.099999999999999645 ) ;
#47587=CARTESIAN_POINT ( 'NONE',  ( -2.271448787322325728E-15, -4.618802153517061804, -5.599999999999999645 ) ) ;
#47729=EDGE_CURVE ( 'NONE', #21005, #16278, #53753, .T. ) ;
#47740=CARTESIAN_POINT ( 'NONE',  ( 4.000000000000003553, 2.309401076758524685, -0.3572655899081733644 ) ) ;
#47943=CIRCLE ( 'NONE', #21919, 4.000000000000000888 ) ;
#48030=EDGE_CURVE ( 'NONE', #51786, #7613, #50776, .T. ) ;
#48077=DIRECTION ( 'NONE',  ( -0.000000000000000000, -0.000000000000000000, 1.000000000000000000 ) ) ;
#48149=DIRECTION ( 'NONE',  ( -1.000000000000000000, 0.000000000000000000, 0.000000000000000000 ) ) ;
#48207=ORIENTED_EDGE ( 'NONE', *, *, #38786, .F. ) ;
#48322=VERTEX_POINT ( 'NONE', #15711 ) ;
#48344=EDGE_CURVE ( 'NONE', #56562, #60958, #55176, .T. ) ;
#48345=CARTESIAN_POINT ( 'NONE',  ( 0.000000000000000000, 0.000000000000000000, 0.000000000000000000 ) ) ;
#48377=DIRECTION ( 'NONE',  ( 0.000000000000000000, 0.000000000000000000, -1.000000000000000000 ) ) ;
#48410=CARTESIAN_POINT ( 'NONE',  ( -2.000000000000009770, 3.464101615137749057, -5.600000000000000533 ) ) ;
#48443=( NAMED_UNIT ( * ) SI_UNIT ( $, .STERADIAN. ) SOLID_ANGLE_UNIT ( ) );
#48509=EDGE_CURVE ( 'NONE', #22420, #48322, #43238, .T. ) ;
#48540=VERTEX_POINT ( 'NONE', #58507 ) ;
#48660=CARTESIAN_POINT ( 'NONE',  ( -7.632783294297951215E-14, -4.618802153517020948, -0.3572655899081733644 ) ) ;
#48737=CARTESIAN_POINT ( 'NONE',  ( 1.321505333908969293, -3.855830693249186147, -5.565789719053443996 ) ) ;
#48760=ORIENTED_EDGE ( 'NONE', *, *, #47231, .T. ) ;
#48773=AXIS2_PLACEMENT_3D ( 'NONE', #2324, #21449, #1701 ) ;
#48832=CARTESIAN_POINT ( 'NONE',  ( -2.099999999999999645, 2.571758278209440971E-16, -0.2800830152838832965 ) ) ;
#48895=CARTESIAN_POINT ( 'NONE',  ( 0.000000000000000000, 0.000000000000000000, -5.574599999999999334 ) ) ;
#48923=EDGE_CURVE ( 'NONE', #48322, #18237, #22250, .T. ) ;
#49053=FACE_OUTER_BOUND ( 'NONE', #44217, .T. ) ;
#49119=FACE_OUTER_BOUND ( 'NONE', #12759, .T. ) ;
#49206=CARTESIAN_POINT ( 'NONE',  ( 2.000000000000027089, 3.464101615137739731, -5.600000000000000533 ) ) ;
#49370=EDGE_CURVE ( 'NONE', #32229, #29392, #3418, .T. ) ;
#49437=CARTESIAN_POINT ( 'NONE',  ( -4.000000000000000000, 0.000000000000000000, -5.599999999999999645 ) ) ;
#49632=ORIENTED_EDGE ( 'NONE', *, *, #26251, .F. ) ;
#49667=CARTESIAN_POINT ( 'NONE',  ( -4.000000000000000000, 0.3904826640788061631, -5.600000000000000533 ) ) ;
#49826=CARTESIAN_POINT ( 'NONE',  ( 4.000000000000003553, 2.309401076758524685, -5.242734410091827613 ) ) ;
#49860=ORIENTED_EDGE ( 'NONE', *, *, #50212, .F. ) ;
#49935=EDGE_CURVE ( 'NONE', #52878, #38564, #55596, .T. ) ;
#50148=ADVANCED_FACE ( 'NONE', ( #10793 ), #9343, .T. ) ;
#50212=EDGE_CURVE ( 'NONE', #26742, #48322, #44397, .T. ) ;
#50237=DIRECTION ( 'NONE',  ( 1.000000000000000000, 0.000000000000000000, 0.000000000000000000 ) ) ;
#50282=ORIENTED_EDGE ( 'NONE', *, *, #9231, .T. ) ;
#50396=EDGE_LOOP ( 'NONE', ( #32188, #44132, #54309, #13067, #53599, #5673 ) ) ;
#50684=CARTESIAN_POINT ( 'NONE',  ( -4.000000000000000000, 2.309401076758496263, -0.3572655899081631503 ) ) ;
#50697=CARTESIAN_POINT ( 'NONE',  ( 1.084202172485504434E-14, 4.618802153517020059, -5.242734410091827613 ) ) ;
#50776=CIRCLE ( 'NONE', #42805, 2.500000000000002220 ) ;
#50802=DIRECTION ( 'NONE',  ( -0.000000000000000000, -0.000000000000000000, 1.000000000000000000 ) ) ;
#50908=DIRECTION ( 'NONE',  ( 0.000000000000000000, 0.000000000000000000, 1.000000000000000000 ) ) ;
#50951=CARTESIAN_POINT ( 'NONE',  ( 4.000000000000004441, 0.7862748000878159171, -0.03447227762756879116 ) ) ;
#50977=( NAMED_UNIT ( * ) SI_UNIT ( $, .STERADIAN. ) SOLID_ANGLE_UNIT ( ) );
#51244=EDGE_CURVE ( 'NONE', #18237, #26742, #2137, .T. ) ;
#51260=DIRECTION ( 'NONE',  ( -1.000000000000000000, 0.000000000000000000, 0.000000000000000000 ) ) ;
#51401=DIRECTION ( 'NONE',  ( 0.8660254037844371533, 0.5000000000000025535, 0.000000000000000000 ) ) ;
#51504=VERTEX_POINT ( 'NONE', #10670 ) ;
#51690=ORIENTED_EDGE ( 'NONE', *, *, #12575, .F. ) ;
#51705=DIRECTION ( 'NONE',  ( 0.000000000000000000, 0.000000000000000000, -1.000000000000000000 ) ) ;
#51784=ORIENTED_EDGE ( 'NONE', *, *, #2755, .T. ) ;
#51786=VERTEX_POINT ( 'NONE', #37579 ) ;
#51860=FILL_AREA_STYLE_COLOUR ( '', #9556 ) ;
#51877=DIRECTION ( 'NONE',  ( -1.000000000000000000, 0.000000000000000000, 0.000000000000000000 ) ) ;
#51922=CARTESIAN_POINT ( 'NONE',  ( -3.344563996438217224, -2.687817229851499068, -0.1586754815285013609 ) ) ;
#51991=CARTESIAN_POINT ( 'NONE',  ( 2.339468227445713921, 3.268109542640642573, 2.447078184617672891E-15 ) ) ;
#52000=CARTESIAN_POINT ( 'NONE',  ( -4.000000000000000000, 2.309401076758496263, -5.599999999999999645 ) ) ;
#52027=CARTESIAN_POINT ( 'NONE',  ( 2.000000000000010658, -3.464101615137748169, -5.600000000000000533 ) ) ;
#52077=DIRECTION ( 'NONE',  ( -0.000000000000000000, -0.000000000000000000, 1.000000000000000000 ) ) ;
#52092=EDGE_LOOP ( 'NONE', ( #48760, #16666, #32567 ) ) ;
#52114=PLANE ( 'NONE',  #57875 ) ;
#52164=AXIS2_PLACEMENT_3D ( 'NONE', #33693, #52769, #9873 ) ;
#52180=ORIENTED_EDGE ( 'NONE', *, *, #11200, .F. ) ;
#52225=FACE_OUTER_BOUND ( 'NONE', #52092, .T. ) ;
#52240=ORIENTED_EDGE ( 'NONE', *, *, #41201, .F. ) ;
#52292=EDGE_CURVE ( 'NONE', #19953, #16278, #8268, .T. ) ;
#52419=FACE_OUTER_BOUND ( 'NONE', #61469, .T. ) ;
#52604=CARTESIAN_POINT ( 'NONE',  ( 3.673643420401899728, 2.497823135841253706, -0.2484800633749943699 ) ) ;
#52683=DIRECTION ( 'NONE',  ( 0.8191520442889896891, 0.000000000000000000, 0.5735764363510490460 ) ) ;
#52704=DIRECTION ( 'NONE',  ( -0.000000000000000000, -0.000000000000000000, 1.000000000000000000 ) ) ;
#52731=EDGE_CURVE ( 'NONE', #7613, #51786, #10469, .T. ) ;
#52759=CYLINDRICAL_SURFACE ( 'NONE', #29225, 2.500000000000002220 ) ;
#52769=DIRECTION ( 'NONE',  ( -0.000000000000000000, -0.000000000000000000, 1.000000000000000000 ) ) ;
#52837=( NAMED_UNIT ( * ) PLANE_ANGLE_UNIT ( ) SI_UNIT ( $, .RADIAN. ) );
#52849=CARTESIAN_POINT ( 'NONE',  ( 2.500000000000000444, 0.000000000000000000, 3.469446951953614189E-15 ) ) ;
#52856=CARTESIAN_POINT ( 'NONE',  ( 3.999999999999990674, -2.309401076758548221, -5.242734410091827613 ) ) ;
#52878=VERTEX_POINT ( 'NONE', #24317 ) ;
#53075=FACE_OUTER_BOUND ( 'NONE', #32503, .T. ) ;
#53115=CARTESIAN_POINT ( 'NONE',  ( 0.000000000000000000, 0.000000000000000000, -5.599999999999999645 ) ) ;
#53156=CYLINDRICAL_SURFACE ( 'NONE', #30743, 2.099999999999999645 ) ;
#53202=DIRECTION ( 'NONE',  ( -0.000000000000000000, -0.000000000000000000, 1.000000000000000000 ) ) ;
#53251=SHAPE_REPRESENTATION ( 'hex nut gradec_iso_ISO - 4034 - M5 - N', ( #14677 ), #12915 ) ;
#53308=ORIENTED_EDGE ( 'NONE', *, *, #21095, .T. ) ;
#53385=CARTESIAN_POINT ( 'NONE',  ( -4.000000000000000000, -1.933795701539610556, -0.2488376576622980119 ) ) ;
#53391=ADVANCED_FACE ( 'NONE', ( #56398 ), #3425, .F. ) ;
#53412=ORIENTED_EDGE ( 'NONE', *, *, #48923, .T. ) ;
#53486=ORIENTED_EDGE ( 'NONE', *, *, #10181, .T. ) ;
#53500=CARTESIAN_POINT ( 'NONE',  ( 0.000000000000000000, 0.000000000000000000, 3.469446951953614189E-15 ) ) ;
#53599=ORIENTED_EDGE ( 'NONE', *, *, #48344, .F. ) ;
#53673=ORIENTED_EDGE ( 'NONE', *, *, #4082, .F. ) ;
#53702=EDGE_LOOP ( 'NONE', ( #53984, #27909, #26970 ) ) ;
#53753=CIRCLE ( 'NONE', #26776, 2.500000000000000444 ) ;
#53801=FACE_BOUND ( 'NONE', #4661, .T. ) ;
#53819=CARTESIAN_POINT ( 'NONE',  ( -2.000000000000009770, 3.464101615137749057, 0.000000000000000000 ) ) ;
#53901=CONICAL_SURFACE ( 'NONE', #39965, 4.000000000000000000, 1.047197551196595855 ) ;
#53984=ORIENTED_EDGE ( 'NONE', *, *, #42518, .T. ) ;
#54111=FACE_OUTER_BOUND ( 'NONE', #57174, .T. ) ;
#54197=ADVANCED_FACE ( 'NONE', ( #26444 ), #29504, .T. ) ;
#54233=CARTESIAN_POINT ( 'NONE',  ( -7.632783294297951215E-14, -4.618802153517020948, -0.3572655899081733644 ) ) ;
#54297=CARTESIAN_POINT ( 'NONE',  ( -4.000000000000000000, -1.549102112939103826, -0.1578953385959410982 ) ) ;
#54309=ORIENTED_EDGE ( 'NONE', *, *, #31052, .T. ) ;
#54381=CARTESIAN_POINT ( 'NONE',  ( -2.000000000000022649, -3.464101615137742396, -5.600000000000000533 ) ) ;
#54688=ORIENTED_EDGE ( 'NONE', *, *, #22515, .T. ) ;
#54717=EDGE_CURVE ( 'NONE', #52878, #48540, #2494, .T. ) ;
#54788=EDGE_CURVE ( 'NONE', #331, #40436, #57771, .T. ) ;
#54825=CARTESIAN_POINT ( 'NONE',  ( 0.000000000000000000, 0.000000000000000000, -5.599999999999999645 ) ) ;
#54917=FACE_OUTER_BOUND ( 'NONE', #3458, .T. ) ;
#54972=CARTESIAN_POINT ( 'NONE',  ( -4.000000000000000000, 1.935983797701083420, -5.350530693383767300 ) ) ;
#55033=DIRECTION ( 'NONE',  ( 0.000000000000000000, 0.000000000000000000, -1.000000000000000000 ) ) ;
#55075=EDGE_CURVE ( 'NONE', #478, #44297, #45063, .T. ) ;
#55175=CARTESIAN_POINT ( 'NONE',  ( 4.000000000000004441, 0.7862748000878170274, -5.565527722372433317 ) ) ;
#55176=B_SPLINE_CURVE_WITH_KNOTS ( 'NONE', 3,
 ( #49206, #44851, #21021, #40162, #16313, #49826 ),
 .UNSPECIFIED., .F., .F.,
 ( 4, 2, 4 ),
 ( 0.002336974151641576809, 0.003500975885716453226, 0.004664977619791330077 ),
 .UNSPECIFIED. ) ;
#55244=DIRECTION ( 'NONE',  ( 0.000000000000000000, 0.000000000000000000, -1.000000000000000000 ) ) ;
#55288=CARTESIAN_POINT ( 'NONE',  ( 2.099999999999999645, 0.000000000000000000, -5.599999999999999645 ) ) ;
#55337=FACE_OUTER_BOUND ( 'NONE', #70, .T. ) ;
#55596=LINE ( 'NONE', #55288, #32344 ) ;
#55653=ORIENTED_EDGE ( 'NONE', *, *, #37422, .T. ) ;
#55656=DIRECTION ( 'NONE',  ( 1.000000000000000000, 0.000000000000000000, 0.000000000000000000 ) ) ;
#55735=VECTOR ( 'NONE', #10278, 1000.000000000000000 ) ;
#55929=EDGE_CURVE ( 'NONE', #29392, #6786, #9076, .T. ) ;
#55942=( NAMED_UNIT ( * ) PLANE_ANGLE_UNIT ( ) SI_UNIT ( $, .RADIAN. ) );
#55948=EDGE_CURVE ( 'NONE', #52878, #7613, #16237, .T. ) ;
#56022=LINE ( 'NONE', #19372, #55735 ) ;
#56048=CONICAL_SURFACE ( 'NONE', #2021, 2.060000000000000941, 0.9599310885968777018 ) ;
#56145=CARTESIAN_POINT ( 'NONE',  ( 4.000000000000003553, -1.933795701539621659, -5.351162342337697275 ) ) ;
#56169=VERTEX_POINT ( 'NONE', #48660 ) ;
#56262=CARTESIAN_POINT ( 'NONE',  ( 4.000000000000003553, 1.935983797701078757, -0.2494693066162350648 ) ) ;
#56398=FACE_OUTER_BOUND ( 'NONE', #12355, .T. ) ;
#56508=AXIS2_PLACEMENT_3D ( 'NONE', #21843, #3326, #8338 ) ;
#56551=EDGE_CURVE ( 'NONE', #60958, #40436, #19338, .T. ) ;
#56562=VERTEX_POINT ( 'NONE', #37221 ) ;
#56577=CARTESIAN_POINT ( 'NONE',  ( 0.000000000000000000, 0.000000000000000000, 0.000000000000000000 ) ) ;
#56595=CONICAL_SURFACE ( 'NONE', #6525, 4.000000000000000000, 1.047197551196595855 ) ;
#56854=B_SPLINE_CURVE_WITH_KNOTS ( 'NONE', 3,
 ( #52856, #849, #43177, #14053 ),
 .UNSPECIFIED., .F., .F.,
 ( 4, 4 ),
 ( 2.380737581782212780E-07, 0.002336974151641520864 ),
 .UNSPECIFIED. ) ;
#56869=EDGE_CURVE ( 'NONE', #14833, #56169, #7376, .T. ) ;
#56886=DIRECTION ( 'NONE',  ( 0.000000000000000000, -0.000000000000000000, 1.000000000000000000 ) ) ;
#56930=DIRECTION ( 'NONE',  ( 1.000000000000000000, 0.000000000000000000, 0.000000000000000000 ) ) ;
#56958=AXIS2_PLACEMENT_3D ( 'NONE', #18166, #28165, #22855 ) ;
#57050=DIRECTION ( 'NONE',  ( 1.000000000000000000, 0.000000000000000000, 0.000000000000000000 ) ) ;
#57057=CARTESIAN_POINT ( 'NONE',  ( 1.318516776095788545, 3.857556137907071747, -5.600000000000003197 ) ) ;
#57138=ORIENTED_EDGE ( 'NONE', *, *, #16924, .T. ) ;
#57174=EDGE_LOOP ( 'NONE', ( #49632, #49860, #1173, #57487, #18480, #58182 ) ) ;
#57213=CARTESIAN_POINT ( 'NONE',  ( -2.000000000000022649, -3.464101615137742396, 0.000000000000000000 ) ) ;
#57285=CARTESIAN_POINT ( 'NONE',  ( 2.000000000000010658, -3.464101615137748169, 0.000000000000000000 ) ) ;
#57487=ORIENTED_EDGE ( 'NONE', *, *, #21706, .F. ) ;
#57598=CARTESIAN_POINT ( 'NONE',  ( -4.000000000000000000, 0.3904826640788011116, -3.430483436379915141E-17 ) ) ;
#57686=ORIENTED_EDGE ( 'NONE', *, *, #21081, .T. ) ;
#57771=B_SPLINE_CURVE_WITH_KNOTS ( 'NONE', 3,
 ( #31866, #60644, #50951, #60965, #56262, #8972 ),
 .UNSPECIFIED., .F., .F.,
 ( 4, 2, 4 ),
 ( 0.006456566858647416578, 0.007625406818786683791, 0.008794246778925951871 ),
 .UNSPECIFIED. ) ;
#57787=CARTESIAN_POINT ( 'NONE',  ( -4.000000000000000000, 2.309401076758531346, -5.242734410091827613 ) ) ;
#57819=DIRECTION ( 'NONE',  ( 0.000000000000000000, 0.000000000000000000, 1.000000000000000000 ) ) ;
#57875=AXIS2_PLACEMENT_3D ( 'NONE', #38362, #19246, #37753 ) ;
#58021=ORIENTED_EDGE ( 'NONE', *, *, #54788, .T. ) ;
#58128=ORIENTED_EDGE ( 'NONE', *, *, #54717, .F. ) ;
#58182=ORIENTED_EDGE ( 'NONE', *, *, #3372, .F. ) ;
#58311=CARTESIAN_POINT ( 'NONE',  ( -0.6543461111163950683, -4.241015250120822699, -0.1391502195351546900 ) ) ;
#58365=DIRECTION ( 'NONE',  ( -1.000000000000000000, 0.000000000000000000, 0.000000000000000000 ) ) ;
#58421=CARTESIAN_POINT ( 'NONE',  ( 0.3263565795980685191, -4.430380094434308802, -5.351519936624961282 ) ) ;
#58507=CARTESIAN_POINT ( 'NONE',  ( -2.099999999999999645, 2.571758278209440971E-16, -5.294516984716111097 ) ) ;
#58582=CARTESIAN_POINT ( 'NONE',  ( -4.000000000000000000, 2.309401076758496263, -5.599999999999999645 ) ) ;
#58631=CIRCLE ( 'NONE', #26642, 4.000000000000000888 ) ;
#58768=ADVANCED_FACE ( 'NONE', ( #9475 ), #42582, .T. ) ;
#58816=ORIENTED_EDGE ( 'NONE', *, *, #2128, .F. ) ;
#58878=AXIS2_PLACEMENT_3D ( 'NONE', #36050, #11608, #59821 ) ;
#58922=CIRCLE ( 'NONE', #56958, 2.099999999999999645 ) ;
#59047=CLOSED_SHELL ( 'NONE', ( #30445, #36091, #4557, #7557, #47208, #776, #59055, #19626, #35937, #43467, #5039, #42304, #37351, #13523, #60108, #58768, #31332, #26035, #15582, #13344, #25536, #9457, #50148, #43080, #54197, #39403, #53391, #16641 ) ) ;
#59055=ADVANCED_FACE ( 'NONE', ( #38869 ), #28500, .T. ) ;
#59076=DIRECTION ( 'NONE',  ( -1.000000000000000000, 0.000000000000000000, 0.000000000000000000 ) ) ;
#59365=CARTESIAN_POINT ( 'NONE',  ( -4.000000000000000000, 1.557668341133520373, -5.440303434304243346 ) ) ;
#59610=CARTESIAN_POINT ( 'NONE',  ( 4.000000000000003553, -0.7779732554280840429, -5.566455648918319454 ) ) ;
#59777=CIRCLE ( 'NONE', #2703, 4.000000000000000000 ) ;
#59821=DIRECTION ( 'NONE',  ( -1.000000000000000000, 0.000000000000000000, 0.000000000000000000 ) ) ;
#59874=B_SPLINE_CURVE_WITH_KNOTS ( 'NONE', 3,
 ( #25199, #53385, #54297, #6064, #777, #24910 ),
 .UNSPECIFIED., .F., .F.,
 ( 4, 2, 4 ),
 ( 0.004120275011746842714, 0.005288420935197119671, 0.006456566858647395761 ),
 .UNSPECIFIED. ) ;
#60035=CARTESIAN_POINT ( 'NONE',  ( -2.339468227445729021, -3.268109542640674547, -5.599999999999982769 ) ) ;
#60108=ADVANCED_FACE ( 'NONE', ( #19222 ), #56595, .T. ) ;
#60338=ORIENTED_EDGE ( 'NONE', *, *, #47231, .F. ) ;
#60466=B_SPLINE_CURVE_WITH_KNOTS ( 'NONE', 3,
 ( #43623, #9767, #57057, #19191 ),
 .UNSPECIFIED., .F., .F.,
 ( 4, 4 ),
 ( 2.380737581618758185E-07, 0.002336974151641576809 ),
 .UNSPECIFIED. ) ;
#60539=EDGE_LOOP ( 'NONE', ( #4834, #37124, #36357, #16680, #19911, #24225 ) ) ;
#60574=CARTESIAN_POINT ( 'NONE',  ( -0.6543461111163939581, -4.241015250120822699, -5.460849780464846148 ) ) ;
#60644=CARTESIAN_POINT ( 'NONE',  ( 4.000000000000003553, 0.3904826640788058856, -2.008738634413572465E-15 ) ) ;
#60805=CARTESIAN_POINT ( 'NONE',  ( -2.271448787322325728E-15, -4.618802153517061804, -5.599999999999999645 ) ) ;
#60807=VECTOR ( 'NONE', #30465, 1000.000000000000000 ) ;
#60825=CARTESIAN_POINT ( 'NONE',  ( -7.459310946700270506E-14, -4.618802153517020948, -5.242734410091827613 ) ) ;
#60828=DIRECTION ( 'NONE',  ( -0.000000000000000000, -0.000000000000000000, 1.000000000000000000 ) ) ;
#60896=CIRCLE ( 'NONE', #58878, 4.000000000000000888 ) ;
#60916=CARTESIAN_POINT ( 'NONE',  ( 2.000000000000010658, -3.464101615137748169, 0.000000000000000000 ) ) ;
#60958=VERTEX_POINT ( 'NONE', #40894 ) ;
#60965=CARTESIAN_POINT ( 'NONE',  ( 4.000000000000003553, 1.557668341133516154, -0.1596965656957575475 ) ) ;
#61077=CARTESIAN_POINT ( 'NONE',  ( 2.000000000000027089, 3.464101615137739731, 0.000000000000000000 ) ) ;
#61326=ORIENTED_EDGE ( 'NONE', *, *, #3237, .T. ) ;
#61387=DIRECTION ( 'NONE',  ( 0.000000000000000000, 0.000000000000000000, 1.000000000000000000 ) ) ;
#61469=EDGE_LOOP ( 'NONE', ( #11297, #7941, #57686, #31246, #19756, #40816 ) ) ;
#61785=ORIENTED_EDGE ( 'NONE', *, *, #52731, .F. ) ;
#61849=AXIS2_PLACEMENT_3D ( 'NONE', #26225, #55033, #51260 ) ;
ENDSEC;
END-ISO-10303-21;
